ISO-10303-21;
HEADER;
FILE_DESCRIPTION (('STEP AP214'),
    '1' );
FILE_NAME ('spur gear_iso_ISO - Spur gear 1M 20T 20PA 5FW ---S20B12H25L8.0S1.step',
    '2026-10-08T13:46:47',
    ( '' ),
    ( '' ),
    'SwSTEP 2.0',
    'SolidWorks 2026',
    '' );
FILE_SCHEMA (( 'AUTOMOTIVE_DESIGN' ));
ENDSEC;

DATA;
#5=DIRECTION ( 'NONE',  ( -1.000000000000000000, 0.000000000000000000, -0.000000000000000000 ) ) ;
#9=AXIS2_PLACEMENT_3D ( 'NONE', #7701, #5884, #15018 ) ;
#14=ADVANCED_FACE ( 'NONE', ( #23177 ), #19348, .T. ) ;
#15=DIRECTION ( 'NONE',  ( -1.000000000000000000, 0.000000000000000000, 0.000000000000000000 ) ) ;
#20=ORIENTED_EDGE ( 'NONE', *, *, #20160, .F. ) ;
#55=LINE ( 'NONE', #5451, #11850 ) ;
#60=DIRECTION ( 'NONE',  ( -1.000000000000000000, -0.000000000000000000, 0.000000000000000000 ) ) ;
#65=DIRECTION ( 'NONE',  ( -1.000000000000000000, -0.000000000000000000, -0.000000000000000000 ) ) ;
#73=ORIENTED_EDGE ( 'NONE', *, *, #16986, .F. ) ;
#83=DIRECTION ( 'NONE',  ( -1.000000000000000000, 0.000000000000000000, 0.000000000000000000 ) ) ;
#95=ORIENTED_EDGE ( 'NONE', *, *, #9004, .T. ) ;
#100=ORIENTED_EDGE ( 'NONE', *, *, #5298, .F. ) ;
#114=( NAMED_UNIT ( * ) PLANE_ANGLE_UNIT ( ) SI_UNIT ( $, .RADIAN. ) );
#122=DIRECTION ( 'NONE',  ( -1.000000000000000000, -0.000000000000000000, 0.000000000000000000 ) ) ;
#126=DIRECTION ( 'NONE',  ( 0.000000000000000000, 0.5877852522924743583, -0.8090169943749467851 ) ) ;
#131=ORIENTED_EDGE ( 'NONE', *, *, #16683, .F. ) ;
#135=ORIENTED_EDGE ( 'NONE', *, *, #23501, .F. ) ;
#136=CIRCLE ( 'NONE', #7427, 8.749000000000002331 ) ;
#150=ADVANCED_FACE ( 'NONE', ( #6674 ), #1255, .T. ) ;
#153=CIRCLE ( 'NONE', #6290, 4.000000000000001776 ) ;
#154=CARTESIAN_POINT ( 'NONE',  ( 0.000000000000000000, -6.807171995660630692, 6.478011392632865295 ) ) ;
#162=CARTESIAN_POINT ( 'NONE',  ( 0.000000000000000000, 8.734705317681626724, 0.4999240074894746311 ) ) ;
#165=CARTESIAN_POINT ( 'NONE',  ( 0.000000000000000000, 0.4999240074895661690, -8.734705317681621395 ) ) ;
#166=CARTESIAN_POINT ( 'NONE',  ( 4.999999999999999112, 8.734705317681626724, -0.4999240074894757413 ) ) ;
#167=ORIENTED_EDGE ( 'NONE', *, *, #18888, .T. ) ;
#210=LINE ( 'NONE', #7541, #1252 ) ;
#212=AXIS2_PLACEMENT_3D ( 'NONE', #2091, #18271, #1855 ) ;
#213=DIRECTION ( 'NONE',  ( -1.000000000000000000, -0.000000000000000000, 0.000000000000000000 ) ) ;
#215=ORIENTED_EDGE ( 'NONE', *, *, #13747, .F. ) ;
#216=EDGE_CURVE ( 'NONE', #1719, #20740, #5490, .T. ) ;
#221=ORIENTED_EDGE ( 'NONE', *, *, #20920, .F. ) ;
#223=ORIENTED_EDGE ( 'NONE', *, *, #14244, .T. ) ;
#226=DIRECTION ( 'NONE',  ( -1.000000000000000000, -0.000000000000000000, 0.000000000000000000 ) ) ;
#239=DIRECTION ( 'NONE',  ( -1.000000000000000000, 0.000000000000000000, 0.000000000000000000 ) ) ;
#241=EDGE_CURVE ( 'NONE', #1931, #14063, #136, .T. ) ;
#250=ORIENTED_EDGE ( 'NONE', *, *, #1042, .T. ) ;
#252=EDGE_CURVE ( 'NONE', #16322, #3084, #16594, .T. ) ;
#255=CIRCLE ( 'NONE', #4097, 8.749000000000002331 ) ;
#266=AXIS2_PLACEMENT_3D ( 'NONE', #5948, #13273, #13627 ) ;
#267=AXIS2_PLACEMENT_3D ( 'NONE', #23534, #5337, #9303 ) ;
#291=DIRECTION ( 'NONE',  ( -1.000000000000000000, 0.000000000000000000, 0.000000000000000000 ) ) ;
#295=CARTESIAN_POINT ( 'NONE',  ( 0.000000000000000000, -10.82112760146737962, 1.975651141462196225 ) ) ;
#299=VERTEX_POINT ( 'NONE', #11106 ) ;
#300=DIRECTION ( 'NONE',  ( 0.000000000000000000, 0.000000000000000000, -1.000000000000000000 ) ) ;
#301=DIRECTION ( 'NONE',  ( -1.000000000000000000, -0.000000000000000000, -0.000000000000000000 ) ) ;
#308=AXIS2_PLACEMENT_3D ( 'NONE', #22558, #8314, #14060 ) ;
#310=EDGE_CURVE ( 'NONE', #17992, #7710, #5573, .T. ) ;
#316=EDGE_CURVE ( 'NONE', #22906, #15640, #20161, .T. ) ;
#325=VECTOR ( 'NONE', #2577, 1000.000000000000000 ) ;
#328=CARTESIAN_POINT ( 'NONE',  ( 2.499999999999999556, 1.464956435139542323, 10.90201369670499076 ) ) ;
#335=FACE_OUTER_BOUND ( 'NONE', #5328, .T. ) ;
#339=CARTESIAN_POINT ( 'NONE',  ( 4.999999999999999112, 0.000000000000000000, 0.000000000000000000 ) ) ;
#346=ORIENTED_EDGE ( 'NONE', *, *, #8932, .T. ) ;
#348=DIRECTION ( 'NONE',  ( 0.000000000000000000, 1.000000000000000000, -0.000000000000000000 ) ) ;
#351=DIRECTION ( 'NONE',  ( 0.000000000000000000, 0.000000000000000000, 1.000000000000000000 ) ) ;
#368=CYLINDRICAL_SURFACE ( 'NONE', #9, 8.749000000000002331 ) ;
#398=AXIS2_PLACEMENT_3D ( 'NONE', #11529, #8386, #10076 ) ;
#402=VERTEX_POINT ( 'NONE', #20872 ) ;
#418=ADVANCED_FACE ( 'NONE', ( #22570 ), #11946, .T. ) ;
#420=DIRECTION ( 'NONE',  ( 1.000000000000000000, 0.000000000000000000, 0.000000000000000000 ) ) ;
#436=ORIENTED_EDGE ( 'NONE', *, *, #2367, .T. ) ;
#443=CARTESIAN_POINT ( 'NONE',  ( 0.000000000000000000, 6.478011392632890164, 6.807171995660607600 ) ) ;
#453=CYLINDRICAL_SURFACE ( 'NONE', #16618, 4.000000000000001776 ) ;
#462=VERTEX_POINT ( 'NONE', #5930 ) ;
#477=CARTESIAN_POINT ( 'NONE',  ( 5.000000000000000888, 5.400000000000000355, -1.000000000000000000 ) ) ;
#478=DIRECTION ( 'NONE',  ( 0.000000000000000000, 0.000000000000000000, 1.000000000000000000 ) ) ;
#492=ORIENTED_EDGE ( 'NONE', *, *, #19288, .T. ) ;
#499=ORIENTED_EDGE ( 'NONE', *, *, #310, .T. ) ;
#502=AXIS2_PLACEMENT_3D ( 'NONE', #19793, #15651, #23149 ) ;
#504=AXIS2_PLACEMENT_3D ( 'NONE', #17379, #9846, #2632 ) ;
#522=ORIENTED_EDGE ( 'NONE', *, *, #19880, .T. ) ;
#537=DIRECTION ( 'NONE',  ( 1.000000000000000000, -0.000000000000000000, -0.000000000000000000 ) ) ;
#538=DIRECTION ( 'NONE',  ( -1.000000000000000000, -0.000000000000000000, 0.000000000000000000 ) ) ;
#544=ORIENTED_EDGE ( 'NONE', *, *, #4528, .T. ) ;
#545=ORIENTED_EDGE ( 'NONE', *, *, #18329, .F. ) ;
#551=EDGE_CURVE ( 'NONE', #19948, #10458, #10853, .T. ) ;
#553=CIRCLE ( 'NONE', #17789, 4.000000000000001776 ) ;
#567=ORIENTED_EDGE ( 'NONE', *, *, #3730, .T. ) ;
#569=DIRECTION ( 'NONE',  ( -1.000000000000000000, 0.000000000000000000, 0.000000000000000000 ) ) ;
#571=DIRECTION ( 'NONE',  ( -1.000000000000000000, -0.000000000000000000, 0.000000000000000000 ) ) ;
#573=CARTESIAN_POINT ( 'NONE',  ( 0.000000000000000000, -3.174628368996134320, 8.152713396088753228 ) ) ;
#574=ADVANCED_FACE ( 'NONE', ( #17777 ), #21577, .F. ) ;
#579=ORIENTED_EDGE ( 'NONE', *, *, #15797, .F. ) ;
#583=ADVANCED_FACE ( 'NONE', ( #22922 ), #6649, .T. ) ;
#584=FACE_OUTER_BOUND ( 'NONE', #22626, .T. ) ;
#591=DIRECTION ( 'NONE',  ( -1.000000000000000000, 0.000000000000000000, 0.000000000000000000 ) ) ;
#609=ORIENTED_EDGE ( 'NONE', *, *, #1017, .T. ) ;
#610=CARTESIAN_POINT ( 'NONE',  ( 4.999999999999999112, -5.538577986808850717, -6.772677083992447500 ) ) ;
#615=EDGE_CURVE ( 'NONE', #9363, #5525, #3178, .T. ) ;
#617=ADVANCED_FACE ( 'NONE', ( #10330 ), #17840, .T. ) ;
#638=ORIENTED_EDGE ( 'NONE', *, *, #18988, .T. ) ;
#670=AXIS2_PLACEMENT_3D ( 'NONE', #10554, #3674, #5368 ) ;
#678=CIRCLE ( 'NONE', #6046, 4.000000000000001776 ) ;
#680=DIRECTION ( 'NONE',  ( -1.000000000000000000, -0.000000000000000000, -0.000000000000000000 ) ) ;
#681=ORIENTED_EDGE ( 'NONE', *, *, #21483, .T. ) ;
#696=STYLED_ITEM ( 'NONE', ( #1788 ), #14725 ) ;
#702=DIRECTION ( 'NONE',  ( -0.000000000000000000, 0.000000000000000000, 1.000000000000000000 ) ) ;
#707=DIRECTION ( 'NONE',  ( -1.000000000000000000, 0.000000000000000000, 0.000000000000000000 ) ) ;
#710=CIRCLE ( 'NONE', #20208, 8.749000000000002331 ) ;
#716=EDGE_LOOP ( 'NONE', ( #13134, #16758, #95, #16262 ) ) ;
#719=LINE ( 'NONE', #4557, #8184 ) ;
#723=EDGE_CURVE ( 'NONE', #9984, #9912, #18309, .T. ) ;
#730=AXIS2_PLACEMENT_3D ( 'NONE', #7144, #14338, #16358 ) ;
#732=CARTESIAN_POINT ( 'NONE',  ( 0.000000000000000000, 0.000000000000000000, 0.000000000000000000 ) ) ;
#737=AXIS2_PLACEMENT_3D ( 'NONE', #5154, #15229, #702 ) ;
#755=ORIENTED_EDGE ( 'NONE', *, *, #2170, .F. ) ;
#762=ORIENTED_EDGE ( 'NONE', *, *, #13154, .F. ) ;
#791=ORIENTED_EDGE ( 'NONE', *, *, #17900, .F. ) ;
#805=DIRECTION ( 'NONE',  ( 0.000000000000000000, 0.000000000000000000, 1.000000000000000000 ) ) ;
#806=DIRECTION ( 'NONE',  ( 0.000000000000000000, 0.000000000000000000, 1.000000000000000000 ) ) ;
#810=CARTESIAN_POINT ( 'NONE',  ( 4.999999999999999112, 0.000000000000000000, 0.000000000000000000 ) ) ;
#812=DIRECTION ( 'NONE',  ( -1.000000000000000000, 0.000000000000000000, 0.000000000000000000 ) ) ;
#817=DIRECTION ( 'NONE',  ( -1.000000000000000000, -0.000000000000000000, 0.000000000000000000 ) ) ;
#820=FACE_OUTER_BOUND ( 'NONE', #22082, .T. ) ;
#827=ORIENTED_EDGE ( 'NONE', *, *, #615, .T. ) ;
#835=CARTESIAN_POINT ( 'NONE',  ( 4.999999999999999112, -5.538577986808850717, -6.772677083992447500 ) ) ;
#843=DIRECTION ( 'NONE',  ( 0.000000000000000000, -0.3090169943749548342, 0.9510565162951509777 ) ) ;
#845=EDGE_CURVE ( 'NONE', #11486, #18141, #210, .T. ) ;
#850=CIRCLE ( 'NONE', #9294, 6.000000000000000888 ) ;
#862=CYLINDRICAL_SURFACE ( 'NONE', #15124, 4.000000000000001776 ) ;
#870=CIRCLE ( 'NONE', #11634, 4.000000000000002665 ) ;
#871=EDGE_CURVE ( 'NONE', #6822, #2402, #16754, .T. ) ;
#872=VERTEX_POINT ( 'NONE', #13066 ) ;
#884=CYLINDRICAL_SURFACE ( 'NONE', #4215, 4.000000000000001776 ) ;
#887=CARTESIAN_POINT ( 'NONE',  ( 4.999999999999999112, 9.241976615262160522, -1.699438267350405818 ) ) ;
#909=ORIENTED_EDGE ( 'NONE', *, *, #22823, .T. ) ;
#919=CARTESIAN_POINT ( 'NONE',  ( 4.999999999999999112, 8.461683424509315543, 2.223716399045600145 ) ) ;
#924=CIRCLE ( 'NONE', #14345, 4.000000000000001776 ) ;
#930=VECTOR ( 'NONE', #15661, 1000.000000000000000 ) ;
#947=DIRECTION ( 'NONE',  ( 0.000000000000000000, 0.000000000000000000, 1.000000000000000000 ) ) ;
#949=AXIS2_PLACEMENT_3D ( 'NONE', #6921, #17468, #12328 ) ;
#952=ORIENTED_EDGE ( 'NONE', *, *, #2709, .F. ) ;
#957=CARTESIAN_POINT ( 'NONE',  ( 4.999999999999999112, 7.958834565716877307, -7.593217523260494595 ) ) ;
#960=ORIENTED_EDGE ( 'NONE', *, *, #723, .F. ) ;
#970=CARTESIAN_POINT ( 'NONE',  ( 0.000000000000000000, 6.807171995660585395, 6.478011392632914145 ) ) ;
#972=EDGE_CURVE ( 'NONE', #299, #5121, #23059, .T. ) ;
#990=VERTEX_POINT ( 'NONE', #7666 ) ;
#992=ORIENTED_EDGE ( 'NONE', *, *, #12431, .F. ) ;
#1002=CARTESIAN_POINT ( 'NONE',  ( 4.999999999999999112, -10.90201369670499787, 1.464956435139505020 ) ) ;
#1011=EDGE_LOOP ( 'NONE', ( #3658, #10518, #13282, #21819 ) ) ;
#1015=EDGE_CURVE ( 'NONE', #11403, #4148, #8182, .T. ) ;
#1017=EDGE_CURVE ( 'NONE', #3902, #22278, #8341, .T. ) ;
#1020=CARTESIAN_POINT ( 'NONE',  ( 0.000000000000000000, -9.314797388894900720, 1.239665997526853580 ) ) ;
#1021=ORIENTED_EDGE ( 'NONE', *, *, #3597, .F. ) ;
#1024=AXIS2_PLACEMENT_3D ( 'NONE', #1199, #17638, #17514 ) ;
#1032=DIRECTION ( 'NONE',  ( 0.000000000000000000, 0.3090169943749481174, -0.9510565162951533091 ) ) ;
#1034=DIRECTION ( 'NONE',  ( -1.000000000000000000, 0.000000000000000000, 0.000000000000000000 ) ) ;
#1039=CARTESIAN_POINT ( 'NONE',  ( 0.000000000000000000, 9.680994141368849171, -5.222868219166749704 ) ) ;
#1040=AXIS2_PLACEMENT_3D ( 'NONE', #6929, #16381, #14603 ) ;
#1042=EDGE_CURVE ( 'NONE', #11624, #2890, #19451, .T. ) ;
#1044=DIRECTION ( 'NONE',  ( 1.000000000000000000, -0.000000000000000000, 0.000000000000000000 ) ) ;
#1046=ORIENTED_EDGE ( 'NONE', *, *, #21323, .F. ) ;
#1048=ORIENTED_EDGE ( 'NONE', *, *, #12159, .F. ) ;
#1056=CIRCLE ( 'NONE', #16771, 11.00000000000000000 ) ;
#1063=VERTEX_POINT ( 'NONE', #1358 ) ;
#1066=DIRECTION ( 'NONE',  ( -1.000000000000000000, -0.000000000000000000, 0.000000000000000000 ) ) ;
#1076=DIRECTION ( 'NONE',  ( 1.000000000000000000, 0.000000000000000000, 0.000000000000000000 ) ) ;
#1087=DIRECTION ( 'NONE',  ( -1.000000000000000000, 0.000000000000000000, 0.000000000000000000 ) ) ;
#1088=VECTOR ( 'NONE', #20183, 1000.000000000000000 ) ;
#1090=FACE_OUTER_BOUND ( 'NONE', #13284, .T. ) ;
#1091=CARTESIAN_POINT ( 'NONE',  ( -10.00000000000000000, 0.000000000000000000, 0.000000000000000000 ) ) ;
#1096=ORIENTED_EDGE ( 'NONE', *, *, #6735, .F. ) ;
#1101=ORIENTED_EDGE ( 'NONE', *, *, #21466, .F. ) ;
#1105=DIRECTION ( 'NONE',  ( -1.000000000000000000, 0.000000000000000000, 0.000000000000000000 ) ) ;
#1108=EDGE_CURVE ( 'NONE', #15525, #19779, #19565, .T. ) ;
#1116=DIRECTION ( 'NONE',  ( -1.000000000000000000, 0.000000000000000000, -0.000000000000000000 ) ) ;
#1135=ORIENTED_EDGE ( 'NONE', *, *, #11327, .F. ) ;
#1139=EDGE_CURVE ( 'NONE', #1949, #8348, #15996, .T. ) ;
#1145=EDGE_CURVE ( 'NONE', #17824, #12317, #15957, .T. ) ;
#1147=CARTESIAN_POINT ( 'NONE',  ( 0.000000000000000000, 0.000000000000000000, 0.000000000000000000 ) ) ;
#1154=DIRECTION ( 'NONE',  ( 0.000000000000000000, 0.000000000000000000, -1.000000000000000000 ) ) ;
#1165=DIRECTION ( 'NONE',  ( -1.000000000000000000, 0.000000000000000000, 0.000000000000000000 ) ) ;
#1174=EDGE_LOOP ( 'NONE', ( #15577, #8700, #10430, #20512 ) ) ;
#1179=CARTESIAN_POINT ( 'NONE',  ( 4.999999999999999112, 0.000000000000000000, 0.000000000000000000 ) ) ;
#1180=DIRECTION ( 'NONE',  ( 0.000000000000000000, 0.000000000000000000, 1.000000000000000000 ) ) ;
#1191=ORIENTED_EDGE ( 'NONE', *, *, #21487, .F. ) ;
#1192=CARTESIAN_POINT ( 'NONE',  ( 0.000000000000000000, 7.347880794884120722E-16, 6.000000000000000888 ) ) ;
#1199=CARTESIAN_POINT ( 'NONE',  ( 4.999999999999999112, 0.000000000000000000, 0.000000000000000000 ) ) ;
#1213=ORIENTED_EDGE ( 'NONE', *, *, #16976, .T. ) ;
#1230=CARTESIAN_POINT ( 'NONE',  ( 2.499999999999999556, -4.762163868918205978, -9.915734732513268312 ) ) ;
#1247=DIRECTION ( 'NONE',  ( 0.000000000000000000, 0.000000000000000000, 1.000000000000000000 ) ) ;
#1252=VECTOR ( 'NONE', #14860, 1000.000000000000000 ) ;
#1255=CYLINDRICAL_SURFACE ( 'NONE', #12424, 8.749000000000002331 ) ;
#1260=PLANE ( 'NONE',  #10933 ) ;
#1262=CLOSED_SHELL ( 'NONE', ( #12173, #18259, #8900, #23265, #5232, #15888, #13041, #16982, #9204, #17816, #574, #17103, #7934, #5546, #10230, #18707, #15440, #22542, #13050, #17709, #6756, #18453, #617, #21807, #2163, #4498, #2772, #13616, #2395, #20898, #18963, #19011, #7497, #10766, #150, #14, #7174, #12851, #22115, #16736, #418, #2742, #8003, #7474, #4089, #21000, #19732, #13311, #23369, #1634, #6162, #12147, #583, #19221, #2764, #10870, #8072, #20362, #16524, #9978, #8833, #16699, #18694, #1640, #10577, #8731, #17549, #11935, #6437, #3995, #20006, #9569, #2734, #16844, #3919, #14186, #11659, #18299, #17450, #6002, #2025, #10895, #14620, #18769, #4674, #21395, #4890, #6632, #5534, #7372, #16124, #23427, #11393, #3371, #17557, #5197 ) ) ;
#1263=DIRECTION ( 'NONE',  ( -1.000000000000000000, -0.000000000000000000, -0.000000000000000000 ) ) ;
#1271=CYLINDRICAL_SURFACE ( 'NONE', #2645, 4.000000000000001776 ) ;
#1274=EDGE_LOOP ( 'NONE', ( #12538, #14783, #7203, #5503 ) ) ;
#1275=LINE ( 'NONE', #10311, #14119 ) ;
#1283=EDGE_LOOP ( 'NONE', ( #5038, #4850, #609, #13055 ) ) ;
#1286=CARTESIAN_POINT ( 'NONE',  ( 2.499999999999999556, -5.222868219166923787, 9.680994141368751471 ) ) ;
#1303=ORIENTED_EDGE ( 'NONE', *, *, #18011, .F. ) ;
#1306=EDGE_CURVE ( 'NONE', #20599, #22213, #19763, .T. ) ;
#1321=EDGE_CURVE ( 'NONE', #12867, #6822, #20025, .T. ) ;
#1333=EDGE_LOOP ( 'NONE', ( #22696, #8411, #579, #16980 ) ) ;
#1338=CIRCLE ( 'NONE', #14763, 8.749000000000000554 ) ;
#1339=CARTESIAN_POINT ( 'NONE',  ( 4.999999999999999112, -4.472189673936728838, -8.264486777890155622 ) ) ;
#1349=DIRECTION ( 'NONE',  ( 0.000000000000000000, 0.000000000000000000, 1.000000000000000000 ) ) ;
#1358=CARTESIAN_POINT ( 'NONE',  ( 0.000000000000000000, -7.593217523260523016, -7.958834565716849774 ) ) ;
#1359=VERTEX_POINT ( 'NONE', #9523 ) ;
#1365=ORIENTED_EDGE ( 'NONE', *, *, #1794, .T. ) ;
#1366=DIRECTION ( 'NONE',  ( 0.000000000000000000, 0.000000000000000000, 1.000000000000000000 ) ) ;
#1381=LINE ( 'NONE', #12443, #16840 ) ;
#1399=DIRECTION ( 'NONE',  ( -1.000000000000000000, -0.000000000000000000, 0.000000000000000000 ) ) ;
#1403=AXIS2_PLACEMENT_3D ( 'NONE', #21864, #5470, #16151 ) ;
#1419=CIRCLE ( 'NONE', #13308, 4.000000000000000888 ) ;
#1425=CIRCLE ( 'NONE', #11801, 4.000000000000001776 ) ;
#1436=EDGE_CURVE ( 'NONE', #17091, #22338, #12550, .T. ) ;
#1437=AXIS2_PLACEMENT_3D ( 'NONE', #12710, #14257, #21515 ) ;
#1444=AXIS2_PLACEMENT_3D ( 'NONE', #22943, #17911, #1247 ) ;
#1448=EDGE_LOOP ( 'NONE', ( #14635, #6191, #18723, #16969 ) ) ;
#1455=EDGE_CURVE ( 'NONE', #6574, #22213, #5240, .T. ) ;
#1457=CARTESIAN_POINT ( 'NONE',  ( 0.000000000000000000, 0.4999240074894452657, 8.734705317681628500 ) ) ;
#1467=DIRECTION ( 'NONE',  ( -1.000000000000000000, 0.000000000000000000, 0.000000000000000000 ) ) ;
#1504=EDGE_CURVE ( 'NONE', #10342, #4211, #2172, .T. ) ;
#1513=CARTESIAN_POINT ( 'NONE',  ( 4.999999999999999112, 8.475820894093034852, -4.057423117305300586 ) ) ;
#1517=CIRCLE ( 'NONE', #19859, 8.749000000000000554 ) ;
#1519=CARTESIAN_POINT ( 'NONE',  ( 4.999999999999999112, 0.000000000000000000, 0.000000000000000000 ) ) ;
#1521=CARTESIAN_POINT ( 'NONE',  ( 4.999999999999999112, 0.000000000000000000, 0.000000000000000000 ) ) ;
#1526=DIRECTION ( 'NONE',  ( -1.000000000000000000, -0.000000000000000000, -0.000000000000000000 ) ) ;
#1537=DIRECTION ( 'NONE',  ( 0.000000000000000000, -0.8090169943749403458, -0.5877852522924831291 ) ) ;
#1539=CARTESIAN_POINT ( 'NONE',  ( 2.499999999999999556, 4.762163868918413812, -9.915734732513168836 ) ) ;
#1543=VERTEX_POINT ( 'NONE', #7216 ) ;
#1548=ORIENTED_EDGE ( 'NONE', *, *, #21156, .T. ) ;
#1549=CYLINDRICAL_SURFACE ( 'NONE', #18581, 11.00000000000000000 ) ;
#1562=DIRECTION ( 'NONE',  ( 0.000000000000000000, 0.5877852522924743583, -0.8090169943749467851 ) ) ;
#1565=CARTESIAN_POINT ( 'NONE',  ( 4.999999999999999112, 0.000000000000000000, 0.000000000000000000 ) ) ;
#1593=EDGE_CURVE ( 'NONE', #17904, #18669, #255, .T. ) ;
#1596=CARTESIAN_POINT ( 'NONE',  ( 4.999999999999999112, 5.222868219166856285, 9.680994141368790551 ) ) ;
#1600=ORIENTED_EDGE ( 'NONE', *, *, #1015, .T. ) ;
#1607=ORIENTED_EDGE ( 'NONE', *, *, #11431, .F. ) ;
#1609=EDGE_LOOP ( 'NONE', ( #3684, #17235, #21402, #18937 ) ) ;
#1611=CARTESIAN_POINT ( 'NONE',  ( 0.000000000000000000, -3.174628368996021521, -8.152713396088794084 ) ) ;
#1619=CIRCLE ( 'NONE', #15049, 4.000000000000001776 ) ;
#1623=CARTESIAN_POINT ( 'NONE',  ( 0.000000000000000000, -7.360373001730951437, 4.729683950898845524 ) ) ;
#1634=ADVANCED_FACE ( 'NONE', ( #14436 ), #8929, .T. ) ;
#1636=CYLINDRICAL_SURFACE ( 'NONE', #20929, 8.749000000000002331 ) ;
#1640=ADVANCED_FACE ( 'NONE', ( #9048 ), #14563, .T. ) ;
#1644=DIRECTION ( 'NONE',  ( 0.000000000000000000, 0.000000000000000000, -1.000000000000000000 ) ) ;
#1645=DIRECTION ( 'NONE',  ( 0.000000000000000000, -0.9510565162951499785, -0.3090169943749581649 ) ) ;
#1653=VECTOR ( 'NONE', #22932, 1000.000000000000000 ) ;
#1654=FACE_OUTER_BOUND ( 'NONE', #10152, .T. ) ;
#1665=EDGE_CURVE ( 'NONE', #19814, #6753, #17778, .T. ) ;
#1668=VERTEX_POINT ( 'NONE', #8568 ) ;
#1693=ORIENTED_EDGE ( 'NONE', *, *, #4155, .F. ) ;
#1698=CIRCLE ( 'NONE', #22751, 8.749000000000002331 ) ;
#1702=CARTESIAN_POINT ( 'NONE',  ( 4.999999999999999112, 6.807171995660675101, -6.478011392632816445 ) ) ;
#1709=ORIENTED_EDGE ( 'NONE', *, *, #11460, .T. ) ;
#1711=FACE_OUTER_BOUND ( 'NONE', #15669, .T. ) ;
#1715=FILL_AREA_STYLE_COLOUR ( '', #12211 ) ;
#1719=VERTEX_POINT ( 'NONE', #8685 ) ;
#1734=VECTOR ( 'NONE', #538, 1000.000000000000000 ) ;
#1742=CIRCLE ( 'NONE', #21616, 11.00000000000000000 ) ;
#1746=VERTEX_POINT ( 'NONE', #3982 ) ;
#1751=ORIENTED_EDGE ( 'NONE', *, *, #3095, .T. ) ;
#1752=FACE_OUTER_BOUND ( 'NONE', #14993, .T. ) ;
#1760=CARTESIAN_POINT ( 'NONE',  ( 0.000000000000000000, -5.538577986808850717, -6.772677083992447500 ) ) ;
#1772=ORIENTED_EDGE ( 'NONE', *, *, #18829, .F. ) ;
#1780=ORIENTED_EDGE ( 'NONE', *, *, #23533, .F. ) ;
#1788=PRESENTATION_STYLE_ASSIGNMENT (( #5277 ) ) ;
#1794=EDGE_CURVE ( 'NONE', #13420, #6899, #7969, .T. ) ;
#1803=VECTOR ( 'NONE', #8957, 1000.000000000000000 ) ;
#1816=CIRCLE ( 'NONE', #2585, 4.000000000000001776 ) ;
#1832=SURFACE_STYLE_FILL_AREA ( #12668 ) ;
#1837=EDGE_CURVE ( 'NONE', #17270, #14716, #4102, .T. ) ;
#1842=AXIS2_PLACEMENT_3D ( 'NONE', #14714, #21971, #12911 ) ;
#1855=DIRECTION ( 'NONE',  ( 0.000000000000000000, 0.000000000000000000, 1.000000000000000000 ) ) ;
#1858=AXIS2_PLACEMENT_3D ( 'NONE', #14634, #16643, #5504 ) ;
#1864=CARTESIAN_POINT ( 'NONE',  ( 4.999999999999999112, 0.000000000000000000, 0.000000000000000000 ) ) ;
#1895=FACE_OUTER_BOUND ( 'NONE', #10910, .T. ) ;
#1897=CARTESIAN_POINT ( 'NONE',  ( 4.999999999999999112, -4.762163868918204201, -9.915734732513268312 ) ) ;
#1905=LINE ( 'NONE', #22251, #16017 ) ;
#1914=AXIS2_PLACEMENT_3D ( 'NONE', #17590, #19709, #1154 ) ;
#1921=FACE_OUTER_BOUND ( 'NONE', #4705, .T. ) ;
#1931=VERTEX_POINT ( 'NONE', #20962 ) ;
#1945=CARTESIAN_POINT ( 'NONE',  ( 4.999999999999999112, -2.223716399045630343, 8.461683424509308438 ) ) ;
#1949=VERTEX_POINT ( 'NONE', #22892 ) ;
#1960=ORIENTED_EDGE ( 'NONE', *, *, #1992, .T. ) ;
#1965=CARTESIAN_POINT ( 'NONE',  ( 4.999999999999999112, 4.057423117305515525, -8.475820894092930047 ) ) ;
#1973=CARTESIAN_POINT ( 'NONE',  ( 0.000000000000000000, 10.90201369670498721, 1.464956435139581403 ) ) ;
#1974=VERTEX_POINT ( 'NONE', #2419 ) ;
#1984=DIRECTION ( 'NONE',  ( 0.000000000000000000, 0.9510565162951521989, 0.3090169943749515591 ) ) ;
#1992=EDGE_CURVE ( 'NONE', #19485, #11205, #3180, .T. ) ;
#2005=EDGE_CURVE ( 'NONE', #19770, #17091, #9326, .T. ) ;
#2006=VERTEX_POINT ( 'NONE', #22655 ) ;
#2013=ORIENTED_EDGE ( 'NONE', *, *, #20277, .T. ) ;
#2025=ADVANCED_FACE ( 'NONE', ( #10000 ), #6023, .T. ) ;
#2034=DIRECTION ( 'NONE',  ( 0.000000000000000000, 0.000000000000000000, 1.000000000000000000 ) ) ;
#2065=ORIENTED_EDGE ( 'NONE', *, *, #4433, .T. ) ;
#2068=VECTOR ( 'NONE', #4163, 1000.000000000000000 ) ;
#2091=CARTESIAN_POINT ( 'NONE',  ( 4.999999999999999112, -8.475820894092946034, -4.057423117305485327 ) ) ;
#2094=DIRECTION ( 'NONE',  ( 1.000000000000000000, -0.000000000000000000, -0.000000000000000000 ) ) ;
#2096=ORIENTED_EDGE ( 'NONE', *, *, #11629, .F. ) ;
#2097=ORIENTED_EDGE ( 'NONE', *, *, #11327, .T. ) ;
#2101=CARTESIAN_POINT ( 'NONE',  ( 4.999999999999999112, 0.000000000000000000, 0.000000000000000000 ) ) ;
#2123=AXIS2_PLACEMENT_3D ( 'NONE', #9081, #3309, #6922 ) ;
#2124=CYLINDRICAL_SURFACE ( 'NONE', #19217, 4.000000000000001776 ) ;
#2138=CARTESIAN_POINT ( 'NONE',  ( 4.999999999999999112, 5.222868219166995729, -9.680994141368715944 ) ) ;
#2142=VERTEX_POINT ( 'NONE', #5281 ) ;
#2143=DIRECTION ( 'NONE',  ( 0.000000000000000000, 0.5877852522924685852, 0.8090169943749506709 ) ) ;
#2163=ADVANCED_FACE ( 'NONE', ( #11826 ), #19328, .T. ) ;
#2170=EDGE_CURVE ( 'NONE', #1668, #21207, #870, .T. ) ;
#2172=CIRCLE ( 'NONE', #20530, 4.000000000000001776 ) ;
#2175=CARTESIAN_POINT ( 'NONE',  ( 5.000000000000000888, 0.000000000000000000, 0.000000000000000000 ) ) ;
#2182=CARTESIAN_POINT ( 'NONE',  ( 4.999999999999999112, 1.975651141462237970, 10.82112760146736896 ) ) ;
#2199=EDGE_LOOP ( 'NONE', ( #18134, #3021, #9568, #10063 ) ) ;
#2215=DIRECTION ( 'NONE',  ( 1.000000000000000000, -0.000000000000000000, -0.000000000000000000 ) ) ;
#2219=ORIENTED_EDGE ( 'NONE', *, *, #12351, .F. ) ;
#2222=AXIS2_PLACEMENT_3D ( 'NONE', #16703, #14936, #7737 ) ;
#2238=DIRECTION ( 'NONE',  ( -1.000000000000000000, 0.000000000000000000, 0.000000000000000000 ) ) ;
#2239=VECTOR ( 'NONE', #10664, 1000.000000000000000 ) ;
#2242=DIRECTION ( 'NONE',  ( -1.000000000000000000, 0.000000000000000000, -0.000000000000000000 ) ) ;
#2243=DIRECTION ( 'NONE',  ( -1.000000000000000000, 0.000000000000000000, 0.000000000000000000 ) ) ;
#2244=DIRECTION ( 'NONE',  ( 0.000000000000000000, 0.8090169943749444537, 0.5877852522924770229 ) ) ;
#2253=DIRECTION ( 'NONE',  ( -1.000000000000000000, 0.000000000000000000, 0.000000000000000000 ) ) ;
#2260=CIRCLE ( 'NONE', #20616, 11.00000000000000000 ) ;
#2264=FACE_OUTER_BOUND ( 'NONE', #6893, .T. ) ;
#2270=CIRCLE ( 'NONE', #14165, 4.000000000000001776 ) ;
#2293=AXIS2_PLACEMENT_3D ( 'NONE', #6505, #6148, #15743 ) ;
#2294=AXIS2_PLACEMENT_3D ( 'NONE', #20762, #4367, #2689 ) ;
#2316=ORIENTED_EDGE ( 'NONE', *, *, #6174, .F. ) ;
#2319=EDGE_CURVE ( 'NONE', #17824, #14427, #19163, .T. ) ;
#2323=FACE_OUTER_BOUND ( 'NONE', #9677, .T. ) ;
#2324=CYLINDRICAL_SURFACE ( 'NONE', #17527, 4.000000000000001776 ) ;
#2327=FACE_OUTER_BOUND ( 'NONE', #11099, .T. ) ;
#2340=VERTEX_POINT ( 'NONE', #20829 ) ;
#2341=DIRECTION ( 'NONE',  ( 0.000000000000000000, 8.881784197001252323E-16, 1.000000000000000000 ) ) ;
#2344=EDGE_CURVE ( 'NONE', #1931, #4288, #12005, .T. ) ;
#2346=EDGE_CURVE ( 'NONE', #6899, #6515, #719, .T. ) ;
#2349=DIRECTION ( 'NONE',  ( -1.000000000000000000, 0.000000000000000000, -0.000000000000000000 ) ) ;
#2367=EDGE_CURVE ( 'NONE', #462, #18141, #3932, .T. ) ;
#2369=DIRECTION ( 'NONE',  ( -1.000000000000000000, 0.000000000000000000, 0.000000000000000000 ) ) ;
#2370=EDGE_CURVE ( 'NONE', #19770, #5947, #8556, .T. ) ;
#2373=DIRECTION ( 'NONE',  ( 0.000000000000000000, 0.000000000000000000, 1.000000000000000000 ) ) ;
#2383=CYLINDRICAL_SURFACE ( 'NONE', #10385, 11.00000000000000000 ) ;
#2392=DIRECTION ( 'NONE',  ( 0.000000000000000000, 0.000000000000000000, 1.000000000000000000 ) ) ;
#2395=ADVANCED_FACE ( 'NONE', ( #11772 ), #21061, .T. ) ;
#2396=DIRECTION ( 'NONE',  ( -1.000000000000000000, 0.000000000000000000, 0.000000000000000000 ) ) ;
#2400=ORIENTED_EDGE ( 'NONE', *, *, #4433, .F. ) ;
#2402=VERTEX_POINT ( 'NONE', #11544 ) ;
#2419=CARTESIAN_POINT ( 'NONE',  ( 4.999999999999999112, 9.680994141368771011, 5.222868219166890036 ) ) ;
#2431=ORIENTED_EDGE ( 'NONE', *, *, #22949, .T. ) ;
#2434=DIRECTION ( 'NONE',  ( 0.000000000000000000, 0.000000000000000000, 1.000000000000000000 ) ) ;
#2436=EDGE_CURVE ( 'NONE', #10458, #7419, #22869, .T. ) ;
#2450=CARTESIAN_POINT ( 'NONE',  ( 0.000000000000000000, 0.000000000000000000, 0.000000000000000000 ) ) ;
#2465=AXIS2_PLACEMENT_3D ( 'NONE', #13620, #6547, #19333 ) ;
#2469=VERTEX_POINT ( 'NONE', #8634 ) ;
#2485=LINE ( 'NONE', #11982, #4039 ) ;
#2488=ORIENTED_EDGE ( 'NONE', *, *, #12030, .F. ) ;
#2490=ORIENTED_EDGE ( 'NONE', *, *, #8240, .F. ) ;
#2498=DIRECTION ( 'NONE',  ( 0.000000000000000000, 0.000000000000000000, 1.000000000000000000 ) ) ;
#2504=CARTESIAN_POINT ( 'NONE',  ( 4.999999999999999112, -9.680994141368730155, -5.222868219166961978 ) ) ;
#2515=ORIENTED_EDGE ( 'NONE', *, *, #17282, .T. ) ;
#2530=CARTESIAN_POINT ( 'NONE',  ( 4.999999999999999112, 9.314797388894893615, 5.239665997526921082 ) ) ;
#2537=VERTEX_POINT ( 'NONE', #6599 ) ;
#2553=AXIS2_PLACEMENT_3D ( 'NONE', #3660, #7517, #22210 ) ;
#2564=CYLINDRICAL_SURFACE ( 'NONE', #2465, 4.000000000000001776 ) ;
#2569=ORIENTED_EDGE ( 'NONE', *, *, #8771, .T. ) ;
#2571=ORIENTED_EDGE ( 'NONE', *, *, #22356, .T. ) ;
#2577=DIRECTION ( 'NONE',  ( 1.000000000000000000, -0.000000000000000000, -0.000000000000000000 ) ) ;
#2580=UNCERTAINTY_MEASURE_WITH_UNIT (LENGTH_MEASURE( 1.000000000000000082E-05 ), #9292, 'distance_accuracy_value', 'NONE');
#2585=AXIS2_PLACEMENT_3D ( 'NONE', #6585, #4894, #17606 ) ;
#2602=LINE ( 'NONE', #9947, #21336 ) ;
#2603=CARTESIAN_POINT ( 'NONE',  ( 4.999999999999999112, -8.475820894092946034, -4.057423117305485327 ) ) ;
#2614=CARTESIAN_POINT ( 'NONE',  ( 0.000000000000000000, -8.734705317681623171, -0.4999240074895356933 ) ) ;
#2632=DIRECTION ( 'NONE',  ( 0.000000000000000000, 0.000000000000000000, -1.000000000000000000 ) ) ;
#2637=ORIENTED_EDGE ( 'NONE', *, *, #18137, .T. ) ;
#2641=ORIENTED_EDGE ( 'NONE', *, *, #15276, .T. ) ;
#2643=VERTEX_POINT ( 'NONE', #11381 ) ;
#2645=AXIS2_PLACEMENT_3D ( 'NONE', #12216, #6930, #10427 ) ;
#2663=CARTESIAN_POINT ( 'NONE',  ( 4.999999999999999112, -4.729683950898817102, -7.360373001730970977 ) ) ;
#2664=AXIS2_PLACEMENT_3D ( 'NONE', #4636, #11970, #22954 ) ;
#2666=CARTESIAN_POINT ( 'NONE',  ( 2.499999999999999556, 5.222868219166856285, 9.680994141368792327 ) ) ;
#2667=ORIENTED_EDGE ( 'NONE', *, *, #14055, .T. ) ;
#2678=AXIS2_PLACEMENT_3D ( 'NONE', #9265, #20596, #20240 ) ;
#2687=AXIS2_PLACEMENT_3D ( 'NONE', #14283, #10696, #17975 ) ;
#2689=DIRECTION ( 'NONE',  ( 0.000000000000000000, 0.000000000000000000, 1.000000000000000000 ) ) ;
#2694=DIRECTION ( 'NONE',  ( -1.000000000000000000, -0.000000000000000000, -0.000000000000000000 ) ) ;
#2709=EDGE_CURVE ( 'NONE', #2825, #7048, #18116, .T. ) ;
#2712=DIRECTION ( 'NONE',  ( 0.000000000000000000, -0.5877852522924624790, -0.8090169943749551118 ) ) ;
#2716=VECTOR ( 'NONE', #19508, 1000.000000000000000 ) ;
#2719=CARTESIAN_POINT ( 'NONE',  ( 4.999999999999999112, 0.000000000000000000, 0.000000000000000000 ) ) ;
#2728=FACE_OUTER_BOUND ( 'NONE', #20664, .T. ) ;
#2731=EDGE_LOOP ( 'NONE', ( #15221, #18067, #14180, #1365 ) ) ;
#2732=CARTESIAN_POINT ( 'NONE',  ( 4.999999999999999112, 0.000000000000000000, 0.000000000000000000 ) ) ;
#2734=ADVANCED_FACE ( 'NONE', ( #335 ), #7669, .T. ) ;
#2740=DIRECTION ( 'NONE',  ( -1.000000000000000000, 0.000000000000000000, -0.000000000000000000 ) ) ;
#2741=DIRECTION ( 'NONE',  ( -1.000000000000000000, 0.000000000000000000, 0.000000000000000000 ) ) ;
#2742=ADVANCED_FACE ( 'NONE', ( #1895 ), #9238, .T. ) ;
#2746=DIRECTION ( 'NONE',  ( -1.000000000000000000, -0.000000000000000000, -0.000000000000000000 ) ) ;
#2747=ORIENTED_EDGE ( 'NONE', *, *, #19021, .F. ) ;
#2764=ADVANCED_FACE ( 'NONE', ( #7196 ), #2124, .T. ) ;
#2772=ADVANCED_FACE ( 'NONE', ( #19975 ), #5851, .T. ) ;
#2777=ORIENTED_EDGE ( 'NONE', *, *, #16217, .T. ) ;
#2778=CARTESIAN_POINT ( 'NONE',  ( 4.999999999999999112, -9.314797388894882957, -1.239665997526988139 ) ) ;
#2799=CARTESIAN_POINT ( 'NONE',  ( 4.999999999999999112, 0.000000000000000000, 0.000000000000000000 ) ) ;
#2825=VERTEX_POINT ( 'NONE', #22609 ) ;
#2833=CYLINDRICAL_SURFACE ( 'NONE', #20097, 4.000000000000001776 ) ;
#2841=DIRECTION ( 'NONE',  ( 0.000000000000000000, 0.000000000000000000, 1.000000000000000000 ) ) ;
#2842=ORIENTED_EDGE ( 'NONE', *, *, #16566, .F. ) ;
#2847=CARTESIAN_POINT ( 'NONE',  ( 4.999999999999999112, -1.464956435139619151, 10.90201369670498188 ) ) ;
#2851=DIRECTION ( 'NONE',  ( 0.000000000000000000, -1.000000000000000000, -1.047444401652939849E-14 ) ) ;
#2864=ORIENTED_EDGE ( 'NONE', *, *, #6501, .T. ) ;
#2867=ORIENTED_EDGE ( 'NONE', *, *, #6589, .F. ) ;
#2871=ORIENTED_EDGE ( 'NONE', *, *, #18062, .T. ) ;
#2874=EDGE_CURVE ( 'NONE', #4915, #1949, #16542, .T. ) ;
#2876=DIRECTION ( 'NONE',  ( 0.000000000000000000, 0.000000000000000000, 1.000000000000000000 ) ) ;
#2890=VERTEX_POINT ( 'NONE', #13771 ) ;
#2891=EDGE_CURVE ( 'NONE', #21750, #23080, #17322, .T. ) ;
#2898=ORIENTED_EDGE ( 'NONE', *, *, #21604, .F. ) ;
#2899=DIRECTION ( 'NONE',  ( 1.000000000000000000, 0.000000000000000000, 0.000000000000000000 ) ) ;
#2903=EDGE_CURVE ( 'NONE', #10755, #17794, #3143, .T. ) ;
#2917=CYLINDRICAL_SURFACE ( 'NONE', #17603, 11.00000000000000000 ) ;
#2926=VERTEX_POINT ( 'NONE', #17352 ) ;
#2930=CARTESIAN_POINT ( 'NONE',  ( 0.000000000000000000, 9.241976615262160522, -1.699438267350405818 ) ) ;
#2931=ORIENTED_EDGE ( 'NONE', *, *, #5867, .T. ) ;
#2932=EDGE_CURVE ( 'NONE', #16281, #14518, #8255, .T. ) ;
#2938=DIRECTION ( 'NONE',  ( 0.000000000000000000, 0.000000000000000000, 1.000000000000000000 ) ) ;
#2943=CARTESIAN_POINT ( 'NONE',  ( 0.000000000000000000, 9.241976615262160522, -1.699438267350405818 ) ) ;
#2944=AXIS2_PLACEMENT_3D ( 'NONE', #21848, #14587, #7620 ) ;
#2945=CARTESIAN_POINT ( 'NONE',  ( 4.999999999999999112, 0.000000000000000000, 0.000000000000000000 ) ) ;
#2954=FACE_OUTER_BOUND ( 'NONE', #12220, .T. ) ;
#2957=VERTEX_POINT ( 'NONE', #1039 ) ;
#2960=EDGE_CURVE ( 'NONE', #10612, #14572, #19583, .T. ) ;
#2984=VERTEX_POINT ( 'NONE', #8497 ) ;
#2991=AXIS2_PLACEMENT_3D ( 'NONE', #16723, #301, #7638 ) ;
#3009=CARTESIAN_POINT ( 'NONE',  ( 4.999999999999999112, -9.915734732513254102, 4.762163868918236176 ) ) ;
#3017=DIRECTION ( 'NONE',  ( 0.000000000000000000, 0.000000000000000000, -1.000000000000000000 ) ) ;
#3020=AXIS2_PLACEMENT_3D ( 'NONE', #3457, #10794, #8993 ) ;
#3021=ORIENTED_EDGE ( 'NONE', *, *, #18793, .F. ) ;
#3029=DIRECTION ( 'NONE',  ( 0.000000000000000000, -0.5877852522924625900, -0.8090169943749552228 ) ) ;
#3038=CIRCLE ( 'NONE', #22548, 8.749000000000002331 ) ;
#3066=VECTOR ( 'NONE', #6423, 1000.000000000000000 ) ;
#3069=EDGE_CURVE ( 'NONE', #16674, #18227, #4758, .T. ) ;
#3074=EDGE_CURVE ( 'NONE', #12101, #18107, #850, .T. ) ;
#3078=DIRECTION ( 'NONE',  ( 0.000000000000000000, 0.000000000000000000, 1.000000000000000000 ) ) ;
#3079=ORIENTED_EDGE ( 'NONE', *, *, #3194, .F. ) ;
#3084=VERTEX_POINT ( 'NONE', #14359 ) ;
#3095=EDGE_CURVE ( 'NONE', #402, #9354, #10182, .T. ) ;
#3097=ORIENTED_EDGE ( 'NONE', *, *, #18520, .F. ) ;
#3100=DIRECTION ( 'NONE',  ( -1.000000000000000000, -0.000000000000000000, 0.000000000000000000 ) ) ;
#3106=DIRECTION ( 'NONE',  ( 0.000000000000000000, 0.000000000000000000, 1.000000000000000000 ) ) ;
#3111=CARTESIAN_POINT ( 'NONE',  ( 0.000000000000000000, 0.000000000000000000, 0.000000000000000000 ) ) ;
#3113=ORIENTED_EDGE ( 'NONE', *, *, #2319, .F. ) ;
#3116=ORIENTED_EDGE ( 'NONE', *, *, #18915, .F. ) ;
#3124=CARTESIAN_POINT ( 'NONE',  ( 0.000000000000000000, -8.475820894093002877, 4.057423117305363647 ) ) ;
#3135=CARTESIAN_POINT ( 'NONE',  ( 0.000000000000000000, 7.593217523260696211, -7.958834565716683684 ) ) ;
#3136=ORIENTED_EDGE ( 'NONE', *, *, #18444, .F. ) ;
#3143=CIRCLE ( 'NONE', #8147, 11.00000000000000000 ) ;
#3148=LINE ( 'NONE', #10492, #20905 ) ;
#3153=DIRECTION ( 'NONE',  ( -1.000000000000000000, 0.000000000000000000, -0.000000000000000000 ) ) ;
#3157=DIRECTION ( 'NONE',  ( 0.000000000000000000, -1.000000000000000000, -1.047444401652939849E-14 ) ) ;
#3175=ORIENTED_EDGE ( 'NONE', *, *, #16288, .F. ) ;
#3178=CIRCLE ( 'NONE', #12771, 4.000000000000000000 ) ;
#3180=CIRCLE ( 'NONE', #7789, 4.000000000000001776 ) ;
#3194=EDGE_CURVE ( 'NONE', #19779, #6822, #9209, .T. ) ;
#3195=CARTESIAN_POINT ( 'NONE',  ( 0.000000000000000000, 9.314797388894893615, 1.239665997526919083 ) ) ;
#3201=ORIENTED_EDGE ( 'NONE', *, *, #6885, .F. ) ;
#3205=EDGE_CURVE ( 'NONE', #1359, #20184, #3438, .T. ) ;
#3216=CYLINDRICAL_SURFACE ( 'NONE', #17277, 8.749000000000002331 ) ;
#3217=ORIENTED_EDGE ( 'NONE', *, *, #3968, .F. ) ;
#3222=DIRECTION ( 'NONE',  ( 0.000000000000000000, 0.000000000000000000, 1.000000000000000000 ) ) ;
#3223=VERTEX_POINT ( 'NONE', #12697 ) ;
#3233=ORIENTED_EDGE ( 'NONE', *, *, #18520, .T. ) ;
#3236=CYLINDRICAL_SURFACE ( 'NONE', #16864, 8.749000000000002331 ) ;
#3242=VECTOR ( 'NONE', #12419, 1000.000000000000000 ) ;
#3244=AXIS2_PLACEMENT_3D ( 'NONE', #7778, #9452, #13415 ) ;
#3254=ORIENTED_EDGE ( 'NONE', *, *, #9004, .F. ) ;
#3262=ORIENTED_EDGE ( 'NONE', *, *, #1139, .F. ) ;
#3265=ORIENTED_EDGE ( 'NONE', *, *, #4531, .T. ) ;
#3277=CIRCLE ( 'NONE', #16676, 8.749000000000002331 ) ;
#3283=ORIENTED_EDGE ( 'NONE', *, *, #20798, .T. ) ;
#3285=DIRECTION ( 'NONE',  ( 1.000000000000000000, 0.000000000000000000, 0.000000000000000000 ) ) ;
#3288=PRESENTATION_STYLE_ASSIGNMENT (( #21473 ) ) ;
#3309=DIRECTION ( 'NONE',  ( -1.000000000000000000, -0.000000000000000000, -0.000000000000000000 ) ) ;
#3319=LINE ( 'NONE', #15809, #2239 ) ;
#3327=EDGE_LOOP ( 'NONE', ( #7869, #12393, #2219, #4023 ) ) ;
#3346=VERTEX_POINT ( 'NONE', #13270 ) ;
#3371=ADVANCED_FACE ( 'NONE', ( #18083 ), #7201, .T. ) ;
#3372=AXIS2_PLACEMENT_3D ( 'NONE', #1020, #8703, #17684 ) ;
#3387=VECTOR ( 'NONE', #10932, 1000.000000000000000 ) ;
#3403=VERTEX_POINT ( 'NONE', #16063 ) ;
#3405=FACE_BOUND ( 'NONE', #3874, .T. ) ;
#3414=DIRECTION ( 'NONE',  ( 0.000000000000000000, 0.000000000000000000, -1.000000000000000000 ) ) ;
#3427=CARTESIAN_POINT ( 'NONE',  ( 4.999999999999999112, 10.90201369670498721, -1.464956435139581403 ) ) ;
#3433=LINE ( 'NONE', #3774, #20450 ) ;
#3438=LINE ( 'NONE', #22211, #23514 ) ;
#3441=AXIS2_PLACEMENT_3D ( 'NONE', #8363, #15681, #22826 ) ;
#3442=DIRECTION ( 'NONE',  ( 0.000000000000000000, 0.3090169943749412895, 0.9510565162951555296 ) ) ;
#3450=VECTOR ( 'NONE', #12747, 1000.000000000000000 ) ;
#3455=VERTEX_POINT ( 'NONE', #14276 ) ;
#3457=CARTESIAN_POINT ( 'NONE',  ( 4.999999999999999112, 9.241976615262133876, 1.699438267350532827 ) ) ;
#3463=CARTESIAN_POINT ( 'NONE',  ( 4.999999999999999112, 0.000000000000000000, 0.000000000000000000 ) ) ;
#3472=CARTESIAN_POINT ( 'NONE',  ( 4.999999999999999112, -5.222868219166923787, 9.680994141368751471 ) ) ;
#3485=DIRECTION ( 'NONE',  ( -1.000000000000000000, -0.000000000000000000, -0.000000000000000000 ) ) ;
#3503=EDGE_LOOP ( 'NONE', ( #5531, #17087, #3727, #17256 ) ) ;
#3506=VERTEX_POINT ( 'NONE', #3472 ) ;
#3521=ORIENTED_EDGE ( 'NONE', *, *, #21761, .F. ) ;
#3522=CARTESIAN_POINT ( 'NONE',  ( 25.00005080000000035, 5.400000000000000355, -1.000000000000000000 ) ) ;
#3527=CARTESIAN_POINT ( 'NONE',  ( 4.999999999999999112, -8.152713396088739017, -3.174628368996162298 ) ) ;
#3528=VERTEX_POINT ( 'NONE', #1192 ) ;
#3531=CARTESIAN_POINT ( 'NONE',  ( 0.000000000000000000, 8.264486777890107660, -4.472189673936815879 ) ) ;
#3535=CARTESIAN_POINT ( 'NONE',  ( 2.499999999999999556, 7.593217523260696211, -7.958834565716683684 ) ) ;
#3536=ORIENTED_EDGE ( 'NONE', *, *, #3784, .F. ) ;
#3537=LINE ( 'NONE', #21605, #5643 ) ;
#3541=CARTESIAN_POINT ( 'NONE',  ( -20.00005079999999680, 0.000000000000000000, 0.000000000000000000 ) ) ;
#3545=DIRECTION ( 'NONE',  ( 1.000000000000000000, 0.000000000000000000, 0.000000000000000000 ) ) ;
#3546=DIRECTION ( 'NONE',  ( -1.000000000000000000, 0.000000000000000000, 0.000000000000000000 ) ) ;
#3547=VERTEX_POINT ( 'NONE', #7788 ) ;
#3552=ORIENTED_EDGE ( 'NONE', *, *, #7740, .T. ) ;
#3572=DIRECTION ( 'NONE',  ( -1.000000000000000000, 0.000000000000000000, 0.000000000000000000 ) ) ;
#3573=AXIS2_PLACEMENT_3D ( 'NONE', #1965, #60, #19939 ) ;
#3574=DIRECTION ( 'NONE',  ( 0.000000000000000000, 0.3090169943749412895, 0.9510565162951555296 ) ) ;
#3575=VERTEX_POINT ( 'NONE', #4056 ) ;
#3580=EDGE_LOOP ( 'NONE', ( #1191, #13275, #5824, #223 ) ) ;
#3597=EDGE_CURVE ( 'NONE', #18669, #8348, #11310, .T. ) ;
#3599=DIRECTION ( 'NONE',  ( -1.000000000000000000, -0.000000000000000000, -0.000000000000000000 ) ) ;
#3614=VECTOR ( 'NONE', #23283, 1000.000000000000000 ) ;
#3621=DIRECTION ( 'NONE',  ( -1.000000000000000000, 0.000000000000000000, 0.000000000000000000 ) ) ;
#3634=VECTOR ( 'NONE', #7399, 1000.000000000000000 ) ;
#3644=CARTESIAN_POINT ( 'NONE',  ( 4.999999999999999112, 6.478011392632982535, -6.807171995660517005 ) ) ;
#3648=CIRCLE ( 'NONE', #17439, 11.00000000000000000 ) ;
#3658=ORIENTED_EDGE ( 'NONE', *, *, #5258, .T. ) ;
#3660=CARTESIAN_POINT ( 'NONE',  ( 4.999999999999999112, 0.000000000000000000, 0.000000000000000000 ) ) ;
#3674=DIRECTION ( 'NONE',  ( -1.000000000000000000, 0.000000000000000000, 0.000000000000000000 ) ) ;
#3684=ORIENTED_EDGE ( 'NONE', *, *, #19014, .F. ) ;
#3690=ORIENTED_EDGE ( 'NONE', *, *, #6931, .F. ) ;
#3700=CARTESIAN_POINT ( 'NONE',  ( 2.499999999999999556, 7.958834565716877307, -7.593217523260497259 ) ) ;
#3704=VECTOR ( 'NONE', #1044, 1000.000000000000000 ) ;
#3705=CIRCLE ( 'NONE', #4093, 11.00000000000000000 ) ;
#3716=AXIS2_PLACEMENT_3D ( 'NONE', #15586, #6225, #17250 ) ;
#3727=ORIENTED_EDGE ( 'NONE', *, *, #3766, .T. ) ;
#3730=EDGE_CURVE ( 'NONE', #18141, #2469, #1742, .T. ) ;
#3732=VECTOR ( 'NONE', #9098, 1000.000000000000000 ) ;
#3737=CARTESIAN_POINT ( 'NONE',  ( 0.000000000000000000, -4.057423117305329896, -8.475820894093020641 ) ) ;
#3746=ORIENTED_EDGE ( 'NONE', *, *, #18358, .T. ) ;
#3755=DIRECTION ( 'NONE',  ( 0.000000000000000000, 0.000000000000000000, 1.000000000000000000 ) ) ;
#3756=VERTEX_POINT ( 'NONE', #573 ) ;
#3762=EDGE_CURVE ( 'NONE', #20778, #3988, #5185, .T. ) ;
#3765=AXIS2_PLACEMENT_3D ( 'NONE', #9479, #20344, #478 ) ;
#3766=EDGE_CURVE ( 'NONE', #11384, #299, #2485, .T. ) ;
#3768=CIRCLE ( 'NONE', #9926, 8.749000000000002331 ) ;
#3774=CARTESIAN_POINT ( 'NONE',  ( 4.999999999999999112, -3.174628368996134320, 8.152713396088753228 ) ) ;
#3783=AXIS2_PLACEMENT_3D ( 'NONE', #12449, #17597, #19598 ) ;
#3784=EDGE_CURVE ( 'NONE', #11205, #15638, #19338, .T. ) ;
#3788=ORIENTED_EDGE ( 'NONE', *, *, #2005, .F. ) ;
#3794=EDGE_CURVE ( 'NONE', #3455, #19485, #17452, .T. ) ;
#3798=DIRECTION ( 'NONE',  ( 0.000000000000000000, 0.000000000000000000, -1.000000000000000000 ) ) ;
#3809=CARTESIAN_POINT ( 'NONE',  ( 4.999999999999999112, -6.807171995660630692, 6.478011392632865295 ) ) ;
#3811=AXIS2_PLACEMENT_3D ( 'NONE', #21020, #8133, #15444 ) ;
#3816=DIRECTION ( 'NONE',  ( 0.000000000000000000, 0.000000000000000000, 1.000000000000000000 ) ) ;
#3830=AXIS2_PLACEMENT_3D ( 'NONE', #443, #7768, #3798 ) ;
#3842=FACE_OUTER_BOUND ( 'NONE', #12830, .T. ) ;
#3855=ORIENTED_EDGE ( 'NONE', *, *, #14702, .F. ) ;
#3874=EDGE_LOOP ( 'NONE', ( #14418, #21594 ) ) ;
#3902=VERTEX_POINT ( 'NONE', #13891 ) ;
#3908=VECTOR ( 'NONE', #23073, 1000.000000000000000 ) ;
#3919=ADVANCED_FACE ( 'NONE', ( #2954 ), #1271, .T. ) ;
#3924=EDGE_CURVE ( 'NONE', #7419, #15377, #22135, .T. ) ;
#3928=ORIENTED_EDGE ( 'NONE', *, *, #6138, .T. ) ;
#3932=CIRCLE ( 'NONE', #4712, 4.000000000000001776 ) ;
#3938=EDGE_CURVE ( 'NONE', #6517, #11847, #5709, .T. ) ;
#3968=EDGE_CURVE ( 'NONE', #10612, #19485, #23339, .T. ) ;
#3971=EDGE_LOOP ( 'NONE', ( #21691, #4448, #8481, #17129 ) ) ;
#3972=EDGE_CURVE ( 'NONE', #1974, #11365, #19091, .T. ) ;
#3982=CARTESIAN_POINT ( 'NONE',  ( 0.000000000000000000, 6.772677083992466152, -5.538577986808826736 ) ) ;
#3988=VERTEX_POINT ( 'NONE', #15820 ) ;
#3995=ADVANCED_FACE ( 'NONE', ( #19504 ), #6818, .T. ) ;
#3997=ORIENTED_EDGE ( 'NONE', *, *, #11431, .T. ) ;
#4000=DIRECTION ( 'NONE',  ( -1.000000000000000000, -0.000000000000000000, -0.000000000000000000 ) ) ;
#4002=VECTOR ( 'NONE', #12473, 1000.000000000000000 ) ;
#4023=ORIENTED_EDGE ( 'NONE', *, *, #8948, .F. ) ;
#4025=CARTESIAN_POINT ( 'NONE',  ( 0.000000000000000000, 6.807171995660675101, -6.478011392632816445 ) ) ;
#4030=UNCERTAINTY_MEASURE_WITH_UNIT (LENGTH_MEASURE( 1.000000000000000082E-05 ), #9057, 'distance_accuracy_value', 'NONE');
#4032=CIRCLE ( 'NONE', #21996, 8.749000000000000554 ) ;
#4039=VECTOR ( 'NONE', #6456, 1000.000000000000000 ) ;
#4041=DIRECTION ( 'NONE',  ( 0.000000000000000000, 0.000000000000000000, 1.000000000000000000 ) ) ;
#4047=DIRECTION ( 'NONE',  ( 0.000000000000000000, -0.8090169943749403458, -0.5877852522924830181 ) ) ;
#4048=AXIS2_PLACEMENT_3D ( 'NONE', #8888, #21660, #15837 ) ;
#4056=CARTESIAN_POINT ( 'NONE',  ( 4.999999999999999112, -9.241976615262146311, 2.300561732649528679 ) ) ;
#4070=CARTESIAN_POINT ( 'NONE',  ( -10.00000000000000000, 0.000000000000000000, 0.000000000000000000 ) ) ;
#4089=ADVANCED_FACE ( 'NONE', ( #13170 ), #453, .T. ) ;
#4093=AXIS2_PLACEMENT_3D ( 'NONE', #5533, #18005, #19905 ) ;
#4097=AXIS2_PLACEMENT_3D ( 'NONE', #21341, #8813, #10620 ) ;
#4102=LINE ( 'NONE', #1945, #21327 ) ;
#4110=ORIENTED_EDGE ( 'NONE', *, *, #216, .T. ) ;
#4118=CARTESIAN_POINT ( 'NONE',  ( 4.999999999999999112, -9.241976615262169403, 1.699438267350339871 ) ) ;
#4119=ORIENTED_EDGE ( 'NONE', *, *, #4646, .T. ) ;
#4130=EDGE_CURVE ( 'NONE', #3403, #23470, #16747, .T. ) ;
#4131=CARTESIAN_POINT ( 'NONE',  ( 4.999999999999999112, 0.000000000000000000, 0.000000000000000000 ) ) ;
#4136=CARTESIAN_POINT ( 'NONE',  ( 2.499999999999999556, -4.762163868918344534, 9.915734732513202587 ) ) ;
#4145=VECTOR ( 'NONE', #22361, 1000.000000000000000 ) ;
#4147=LINE ( 'NONE', #18764, #4505 ) ;
#4148=VERTEX_POINT ( 'NONE', #22235 ) ;
#4153=AXIS2_PLACEMENT_3D ( 'NONE', #4070, #4426, #20704 ) ;
#4155=EDGE_CURVE ( 'NONE', #6665, #17502, #924, .T. ) ;
#4163=DIRECTION ( 'NONE',  ( -1.000000000000000000, 0.000000000000000000, 0.000000000000000000 ) ) ;
#4171=ORIENTED_EDGE ( 'NONE', *, *, #14972, .F. ) ;
#4172=CIRCLE ( 'NONE', #6478, 4.000000000000001776 ) ;
#4173=FACE_OUTER_BOUND ( 'NONE', #11783, .T. ) ;
#4179=EDGE_LOOP ( 'NONE', ( #6639, #21174, #6491, #14240 ) ) ;
#4191=ORIENTED_EDGE ( 'NONE', *, *, #14406, .F. ) ;
#4193=CARTESIAN_POINT ( 'NONE',  ( 4.999999999999999112, 4.057423117305393845, 8.475820894092990443 ) ) ;
#4197=FACE_OUTER_BOUND ( 'NONE', #14096, .T. ) ;
#4211=VERTEX_POINT ( 'NONE', #8249 ) ;
#4214=CIRCLE ( 'NONE', #15282, 4.000000000000000000 ) ;
#4215=AXIS2_PLACEMENT_3D ( 'NONE', #13730, #6651, #12171 ) ;
#4220=AXIS2_PLACEMENT_3D ( 'NONE', #14829, #22083, #300 ) ;
#4222=CIRCLE ( 'NONE', #8450, 4.000000000000001776 ) ;
#4227=DIRECTION ( 'NONE',  ( -1.000000000000000000, 0.000000000000000000, -0.000000000000000000 ) ) ;
#4235=DIRECTION ( 'NONE',  ( 0.000000000000000000, -0.5877852522924624790, -0.8090169943749553338 ) ) ;
#4252=VECTOR ( 'NONE', #9808, 1000.000000000000000 ) ;
#4254=CARTESIAN_POINT ( 'NONE',  ( 4.999999999999999112, -9.241976615262146311, -1.699438267350473097 ) ) ;
#4288=VERTEX_POINT ( 'NONE', #20737 ) ;
#4297=AXIS2_PLACEMENT_3D ( 'NONE', #6212, #2369, #13295 ) ;
#4305=DIRECTION ( 'NONE',  ( 0.000000000000000000, 0.000000000000000000, 1.000000000000000000 ) ) ;
#4314=DIRECTION ( 'NONE',  ( -1.000000000000000000, 0.000000000000000000, 0.000000000000000000 ) ) ;
#4327=CARTESIAN_POINT ( 'NONE',  ( 4.999999999999999112, -8.461683424509331530, 2.223716399045538861 ) ) ;
#4344=DIRECTION ( 'NONE',  ( -1.000000000000000000, 0.000000000000000000, 0.000000000000000000 ) ) ;
#4348=ORIENTED_EDGE ( 'NONE', *, *, #20475, .T. ) ;
#4357=EDGE_LOOP ( 'NONE', ( #14455, #4782, #19653, #9352 ) ) ;
#4367=DIRECTION ( 'NONE',  ( -1.000000000000000000, -0.000000000000000000, 0.000000000000000000 ) ) ;
#4378=CIRCLE ( 'NONE', #22784, 6.000000000000000888 ) ;
#4401=EDGE_CURVE ( 'NONE', #5267, #19658, #5133, .T. ) ;
#4403=ORIENTED_EDGE ( 'NONE', *, *, #6589, .T. ) ;
#4404=CARTESIAN_POINT ( 'NONE',  ( 4.999999999999999112, 5.538577986808997267, -6.772677083992326708 ) ) ;
#4409=CARTESIAN_POINT ( 'NONE',  ( 4.999999999999999112, -0.4999240074895051067, 8.734705317681624948 ) ) ;
#4410=DIRECTION ( 'NONE',  ( -1.000000000000000000, 0.000000000000000000, 0.000000000000000000 ) ) ;
#4426=DIRECTION ( 'NONE',  ( -1.000000000000000000, -0.000000000000000000, -0.000000000000000000 ) ) ;
#4427=CIRCLE ( 'NONE', #14003, 11.00000000000000000 ) ;
#4432=DIRECTION ( 'NONE',  ( -1.000000000000000000, 0.000000000000000000, 0.000000000000000000 ) ) ;
#4433=EDGE_CURVE ( 'NONE', #14063, #1063, #153, .T. ) ;
#4448=ORIENTED_EDGE ( 'NONE', *, *, #7466, .F. ) ;
#4491=ORIENTED_EDGE ( 'NONE', *, *, #16413, .F. ) ;
#4496=ORIENTED_EDGE ( 'NONE', *, *, #10595, .F. ) ;
#4497=AXIS2_PLACEMENT_3D ( 'NONE', #12586, #12816, #1645 ) ;
#4498=ADVANCED_FACE ( 'NONE', ( #17524 ), #22657, .T. ) ;
#4505=VECTOR ( 'NONE', #2349, 1000.000000000000000 ) ;
#4512=AXIS2_PLACEMENT_3D ( 'NONE', #6107, #18910, #2498 ) ;
#4517=DIRECTION ( 'NONE',  ( -1.000000000000000000, 0.000000000000000000, -0.000000000000000000 ) ) ;
#4518=CIRCLE ( 'NONE', #17914, 4.000000000000001776 ) ;
#4528=EDGE_CURVE ( 'NONE', #1949, #3403, #22264, .T. ) ;
#4529=LINE ( 'NONE', #14000, #3704 ) ;
#4531=EDGE_CURVE ( 'NONE', #6311, #402, #1619, .T. ) ;
#4535=ORIENTED_EDGE ( 'NONE', *, *, #13607, .T. ) ;
#4552=VECTOR ( 'NONE', #8990, 1000.000000000000000 ) ;
#4556=CYLINDRICAL_SURFACE ( 'NONE', #14398, 4.000000000000001776 ) ;
#4557=CARTESIAN_POINT ( 'NONE',  ( 2.499999999999999556, -7.958834565716711218, -7.593217523260672230 ) ) ;
#4560=ORIENTED_EDGE ( 'NONE', *, *, #9865, .F. ) ;
#4561=ORIENTED_EDGE ( 'NONE', *, *, #7671, .T. ) ;
#4567=EDGE_CURVE ( 'NONE', #14572, #22615, #18079, .T. ) ;
#4577=FACE_OUTER_BOUND ( 'NONE', #5978, .T. ) ;
#4588=CIRCLE ( 'NONE', #22924, 4.000000000000000000 ) ;
#4598=CARTESIAN_POINT ( 'NONE',  ( -20.00005079999999680, 5.400000000000000355, 1.000000000000000000 ) ) ;
#4601=DIRECTION ( 'NONE',  ( -1.000000000000000000, -0.000000000000000000, 0.000000000000000000 ) ) ;
#4613=VECTOR ( 'NONE', #15, 1000.000000000000000 ) ;
#4620=CARTESIAN_POINT ( 'NONE',  ( 4.999999999999999112, 0.000000000000000000, 0.000000000000000000 ) ) ;
#4621=DIRECTION ( 'NONE',  ( -1.000000000000000000, -0.000000000000000000, -0.000000000000000000 ) ) ;
#4623=LINE ( 'NONE', #11956, #4990 ) ;
#4629=VERTEX_POINT ( 'NONE', #8660 ) ;
#4631=AXIS2_PLACEMENT_3D ( 'NONE', #17620, #5379, #1537 ) ;
#4636=CARTESIAN_POINT ( 'NONE',  ( 4.999999999999999112, 0.000000000000000000, 0.000000000000000000 ) ) ;
#4641=DIRECTION ( 'NONE',  ( 0.000000000000000000, 0.8090169943749446757, 0.5877852522924770229 ) ) ;
#4644=CARTESIAN_POINT ( 'NONE',  ( 4.999999999999999112, 5.538577986808997267, -6.772677083992326708 ) ) ;
#4646=EDGE_CURVE ( 'NONE', #4148, #872, #10827, .T. ) ;
#4647=VERTEX_POINT ( 'NONE', #21554 ) ;
#4654=ORIENTED_EDGE ( 'NONE', *, *, #23575, .F. ) ;
#4671=DIRECTION ( 'NONE',  ( -1.000000000000000000, -0.000000000000000000, 0.000000000000000000 ) ) ;
#4674=ADVANCED_FACE ( 'NONE', ( #1921 ), #7699, .T. ) ;
#4677=ORIENTED_EDGE ( 'NONE', *, *, #17117, .F. ) ;
#4685=LINE ( 'NONE', #15842, #9610 ) ;
#4702=EDGE_CURVE ( 'NONE', #19814, #21750, #7004, .T. ) ;
#4704=DIRECTION ( 'NONE',  ( 1.000000000000000000, -0.000000000000000000, -0.000000000000000000 ) ) ;
#4705=EDGE_LOOP ( 'NONE', ( #2637, #14161, #6964, #16870 ) ) ;
#4712=AXIS2_PLACEMENT_3D ( 'NONE', #15481, #1066, #15244 ) ;
#4731=CARTESIAN_POINT ( 'NONE',  ( 0.000000000000000000, 7.958834565716877307, -7.593217523260497259 ) ) ;
#4743=DIRECTION ( 'NONE',  ( 0.000000000000000000, 0.000000000000000000, -1.000000000000000000 ) ) ;
#4758=LINE ( 'NONE', #21503, #22262 ) ;
#4768=DIRECTION ( 'NONE',  ( 0.000000000000000000, 0.000000000000000000, 1.000000000000000000 ) ) ;
#4769=CIRCLE ( 'NONE', #11692, 4.000000000000000888 ) ;
#4776=DIRECTION ( 'NONE',  ( 0.000000000000000000, 0.5877852522924743583, -0.8090169943749466741 ) ) ;
#4782=ORIENTED_EDGE ( 'NONE', *, *, #1455, .F. ) ;
#4787=DIRECTION ( 'NONE',  ( 0.000000000000000000, 0.9510565162951523099, 0.3090169943749515591 ) ) ;
#4793=ORIENTED_EDGE ( 'NONE', *, *, #13206, .T. ) ;
#4827=ORIENTED_EDGE ( 'NONE', *, *, #21792, .T. ) ;
#4838=CARTESIAN_POINT ( 'NONE',  ( 0.000000000000000000, 9.314797388894893615, 1.239665997526919083 ) ) ;
#4846=DIRECTION ( 'NONE',  ( -1.000000000000000000, 0.000000000000000000, 0.000000000000000000 ) ) ;
#4850=ORIENTED_EDGE ( 'NONE', *, *, #13903, .T. ) ;
#4851=ORIENTED_EDGE ( 'NONE', *, *, #13083, .F. ) ;
#4862=CIRCLE ( 'NONE', #18300, 8.749000000000002331 ) ;
#4875=DIRECTION ( 'NONE',  ( -1.000000000000000000, 0.000000000000000000, -0.000000000000000000 ) ) ;
#4880=ORIENTED_EDGE ( 'NONE', *, *, #12990, .T. ) ;
#4890=ADVANCED_FACE ( 'NONE', ( #15368 ), #4556, .T. ) ;
#4894=DIRECTION ( 'NONE',  ( -1.000000000000000000, 0.000000000000000000, 0.000000000000000000 ) ) ;
#4897=CIRCLE ( 'NONE', #17155, 4.000000000000002665 ) ;
#4915=VERTEX_POINT ( 'NONE', #13559 ) ;
#4945=DIRECTION ( 'NONE',  ( 1.000000000000000000, 0.000000000000000000, 0.000000000000000000 ) ) ;
#4950=DIRECTION ( 'NONE',  ( 0.000000000000000000, -1.000000000000000000, -1.040834085586083783E-14 ) ) ;
#4956=DIRECTION ( 'NONE',  ( 0.000000000000000000, 0.000000000000000000, 1.000000000000000000 ) ) ;
#4970=ORIENTED_EDGE ( 'NONE', *, *, #15696, .T. ) ;
#4972=DIRECTION ( 'NONE',  ( -1.000000000000000000, -0.000000000000000000, 0.000000000000000000 ) ) ;
#4975=CIRCLE ( 'NONE', #20236, 8.749000000000002331 ) ;
#4977=EDGE_CURVE ( 'NONE', #20778, #14063, #6239, .T. ) ;
#4978=ORIENTED_EDGE ( 'NONE', *, *, #10808, .F. ) ;
#4990=VECTOR ( 'NONE', #22447, 1000.000000000000000 ) ;
#4993=DIRECTION ( 'NONE',  ( -1.000000000000000000, 0.000000000000000000, 0.000000000000000000 ) ) ;
#5002=CARTESIAN_POINT ( 'NONE',  ( 4.999999999999999112, -10.82112760146734765, -1.975651141462353211 ) ) ;
#5019=EDGE_LOOP ( 'NONE', ( #10948, #2490, #2747, #14151 ) ) ;
#5021=LINE ( 'NONE', #12350, #5319 ) ;
#5022=CYLINDRICAL_SURFACE ( 'NONE', #7250, 4.000000000000001776 ) ;
#5033=CARTESIAN_POINT ( 'NONE',  ( 0.000000000000000000, -4.762163868918344534, 9.915734732513202587 ) ) ;
#5036=ORIENTED_EDGE ( 'NONE', *, *, #18988, .F. ) ;
#5038=ORIENTED_EDGE ( 'NONE', *, *, #5686, .F. ) ;
#5043=DIRECTION ( 'NONE',  ( -1.000000000000000000, 0.000000000000000000, 0.000000000000000000 ) ) ;
#5053=EDGE_LOOP ( 'NONE', ( #6751, #5225, #346, #14833 ) ) ;
#5065=VERTEX_POINT ( 'NONE', #20322 ) ;
#5070=CARTESIAN_POINT ( 'NONE',  ( 4.999999999999997335, 3.872983346207417021, -1.000000000000000000 ) ) ;
#5088=DIRECTION ( 'NONE',  ( -1.000000000000000000, -0.000000000000000000, -0.000000000000000000 ) ) ;
#5101=EDGE_CURVE ( 'NONE', #22551, #19381, #20478, .T. ) ;
#5112=CARTESIAN_POINT ( 'NONE',  ( 0.000000000000000000, -1.975651141462315463, 10.82112760146735475 ) ) ;
#5115=DIRECTION ( 'NONE',  ( 0.000000000000000000, 0.000000000000000000, 1.000000000000000000 ) ) ;
#5121=VERTEX_POINT ( 'NONE', #10061 ) ;
#5126=LINE ( 'NONE', #23449, #3732 ) ;
#5130=DIRECTION ( 'NONE',  ( -1.000000000000000000, 0.000000000000000000, 0.000000000000000000 ) ) ;
#5132=CYLINDRICAL_SURFACE ( 'NONE', #22529, 8.749000000000002331 ) ;
#5133=CIRCLE ( 'NONE', #17393, 11.00000000000000000 ) ;
#5154=CARTESIAN_POINT ( 'NONE',  ( 5.000000000000000000, 0.000000000000000000, 0.000000000000000000 ) ) ;
#5185=CIRCLE ( 'NONE', #18570, 4.000000000000001776 ) ;
#5189=CARTESIAN_POINT ( 'NONE',  ( 4.999999999999999112, 4.762163868918412923, -9.915734732513167060 ) ) ;
#5191=DIRECTION ( 'NONE',  ( -1.000000000000000000, -0.000000000000000000, 0.000000000000000000 ) ) ;
#5197=ADVANCED_FACE ( 'NONE', ( #13886 ), #20687, .T. ) ;
#5201=ORIENTED_EDGE ( 'NONE', *, *, #23501, .T. ) ;
#5225=ORIENTED_EDGE ( 'NONE', *, *, #23090, .F. ) ;
#5230=VERTEX_POINT ( 'NONE', #4644 ) ;
#5232=ADVANCED_FACE ( 'NONE', ( #11978 ), #2833, .T. ) ;
#5240=CIRCLE ( 'NONE', #15607, 11.00000000000000000 ) ;
#5241=DIRECTION ( 'NONE',  ( 0.000000000000000000, 0.000000000000000000, 1.000000000000000000 ) ) ;
#5253=AXIS2_PLACEMENT_3D ( 'NONE', #10069, #20693, #18794 ) ;
#5256=ORIENTED_EDGE ( 'NONE', *, *, #18296, .T. ) ;
#5258=EDGE_CURVE ( 'NONE', #2469, #1543, #6683, .T. ) ;
#5267=VERTEX_POINT ( 'NONE', #5112 ) ;
#5268=FACE_OUTER_BOUND ( 'NONE', #13397, .T. ) ;
#5271=CIRCLE ( 'NONE', #18649, 4.000000000000000888 ) ;
#5274=FACE_OUTER_BOUND ( 'NONE', #14776, .T. ) ;
#5277=SURFACE_STYLE_USAGE ( .BOTH. , #7086 ) ;
#5281=CARTESIAN_POINT ( 'NONE',  ( 0.000000000000000000, 3.174628368996190719, -8.152713396088728359 ) ) ;
#5289=CARTESIAN_POINT ( 'NONE',  ( 4.999999999999999112, -9.314797388894900720, 1.239665997526853580 ) ) ;
#5291=ORIENTED_EDGE ( 'NONE', *, *, #6200, .T. ) ;
#5294=ORIENTED_EDGE ( 'NONE', *, *, #11158, .F. ) ;
#5298=EDGE_CURVE ( 'NONE', #10244, #22841, #8853, .T. ) ;
#5319=VECTOR ( 'NONE', #2740, 1000.000000000000000 ) ;
#5322=CARTESIAN_POINT ( 'NONE',  ( 4.999999999999999112, -9.241976615262146311, 2.300561732649528679 ) ) ;
#5323=ORIENTED_EDGE ( 'NONE', *, *, #3924, .T. ) ;
#5328=EDGE_LOOP ( 'NONE', ( #5201, #3265, #1751, #7163 ) ) ;
#5331=CIRCLE ( 'NONE', #23687, 11.00000000000000000 ) ;
#5335=VERTEX_POINT ( 'NONE', #17931 ) ;
#5337=DIRECTION ( 'NONE',  ( 1.000000000000000000, 0.000000000000000000, 0.000000000000000000 ) ) ;
#5342=DIRECTION ( 'NONE',  ( 0.000000000000000000, -0.8090169943749530024, 0.5877852522924653655 ) ) ;
#5350=ORIENTED_EDGE ( 'NONE', *, *, #9801, .T. ) ;
#5360=ORIENTED_EDGE ( 'NONE', *, *, #9865, .T. ) ;
#5367=FACE_OUTER_BOUND ( 'NONE', #21920, .T. ) ;
#5368=DIRECTION ( 'NONE',  ( 0.000000000000000000, 0.000000000000000000, 1.000000000000000000 ) ) ;
#5369=CARTESIAN_POINT ( 'NONE',  ( 0.000000000000000000, 0.000000000000000000, 0.000000000000000000 ) ) ;
#5370=ORIENTED_EDGE ( 'NONE', *, *, #14340, .T. ) ;
#5377=CIRCLE ( 'NONE', #18768, 8.749000000000000554 ) ;
#5379=DIRECTION ( 'NONE',  ( -1.000000000000000000, -0.000000000000000000, 0.000000000000000000 ) ) ;
#5380=CIRCLE ( 'NONE', #18771, 4.000000000000002665 ) ;
#5382=DIRECTION ( 'NONE',  ( 1.000000000000000000, -0.000000000000000000, 0.000000000000000000 ) ) ;
#5392=ORIENTED_EDGE ( 'NONE', *, *, #845, .T. ) ;
#5395=CARTESIAN_POINT ( 'NONE',  ( 2.499999999999999556, 5.222868219166995729, -9.680994141368717720 ) ) ;
#5401=CARTESIAN_POINT ( 'NONE',  ( 0.000000000000000000, -9.241976615262146311, -1.699438267350473097 ) ) ;
#5406=CARTESIAN_POINT ( 'NONE',  ( 4.999999999999999112, 0.000000000000000000, 0.000000000000000000 ) ) ;
#5438=DIRECTION ( 'NONE',  ( 0.000000000000000000, 0.000000000000000000, -1.000000000000000000 ) ) ;
#5441=( NAMED_UNIT ( * ) PLANE_ANGLE_UNIT ( ) SI_UNIT ( $, .RADIAN. ) );
#5449=CARTESIAN_POINT ( 'NONE',  ( -10.00000000000000000, 0.000000000000000000, 0.000000000000000000 ) ) ;
#5450=ORIENTED_EDGE ( 'NONE', *, *, #20433, .F. ) ;
#5451=CARTESIAN_POINT ( 'NONE',  ( 2.499999999999999556, 1.464956435139696644, -10.90201369670497122 ) ) ;
#5452=DIRECTION ( 'NONE',  ( 1.000000000000000000, -0.000000000000000000, 0.000000000000000000 ) ) ;
#5455=EDGE_CURVE ( 'NONE', #20184, #11236, #4862, .T. ) ;
#5457=EDGE_CURVE ( 'NONE', #19658, #9455, #18397, .T. ) ;
#5463=CARTESIAN_POINT ( 'NONE',  ( 4.999999999999999112, 0.000000000000000000, 0.000000000000000000 ) ) ;
#5470=DIRECTION ( 'NONE',  ( -1.000000000000000000, 0.000000000000000000, -0.000000000000000000 ) ) ;
#5482=DIRECTION ( 'NONE',  ( 0.000000000000000000, 0.000000000000000000, 1.000000000000000000 ) ) ;
#5483=ORIENTED_EDGE ( 'NONE', *, *, #22260, .T. ) ;
#5489=FACE_OUTER_BOUND ( 'NONE', #1283, .T. ) ;
#5490=CIRCLE ( 'NONE', #3573, 4.000000000000001776 ) ;
#5497=DIRECTION ( 'NONE',  ( -1.000000000000000000, -0.000000000000000000, 0.000000000000000000 ) ) ;
#5503=ORIENTED_EDGE ( 'NONE', *, *, #15949, .T. ) ;
#5504=DIRECTION ( 'NONE',  ( 0.000000000000000000, 0.5877852522924688072, 0.8090169943749507819 ) ) ;
#5508=CARTESIAN_POINT ( 'NONE',  ( 4.999999999999999112, 10.90201369670498721, 1.464956435139581403 ) ) ;
#5510=( LENGTH_UNIT ( ) NAMED_UNIT ( * ) SI_UNIT ( .MILLI., .METRE. ) );
#5518=CARTESIAN_POINT ( 'NONE',  ( 4.999999999999999112, -8.264486777890077462, -4.472189673936873611 ) ) ;
#5520=DIRECTION ( 'NONE',  ( -1.000000000000000000, 0.000000000000000000, -0.000000000000000000 ) ) ;
#5525=VERTEX_POINT ( 'NONE', #5584 ) ;
#5531=ORIENTED_EDGE ( 'NONE', *, *, #12431, .T. ) ;
#5533=CARTESIAN_POINT ( 'NONE',  ( 0.000000000000000000, 0.000000000000000000, 0.000000000000000000 ) ) ;
#5534=ADVANCED_FACE ( 'NONE', ( #20412 ), #9432, .T. ) ;
#5537=AXIS2_PLACEMENT_3D ( 'NONE', #8226, #6421, #13737 ) ;
#5546=ADVANCED_FACE ( 'NONE', ( #11233 ), #7403, .T. ) ;
#5551=EDGE_CURVE ( 'NONE', #15377, #20516, #15215, .T. ) ;
#5555=AXIS2_PLACEMENT_3D ( 'NONE', #11519, #812, #2373 ) ;
#5558=CIRCLE ( 'NONE', #9780, 4.000000000000002665 ) ;
#5570=VECTOR ( 'NONE', #16943, 1000.000000000000000 ) ;
#5573=LINE ( 'NONE', #12900, #8569 ) ;
#5581=EDGE_LOOP ( 'NONE', ( #11162, #14360, #3746, #3521 ) ) ;
#5584=CARTESIAN_POINT ( 'NONE',  ( -20.00005079999999680, 3.872983346207417021, -1.000000000000000000 ) ) ;
#5591=ORIENTED_EDGE ( 'NONE', *, *, #12863, .T. ) ;
#5600=CARTESIAN_POINT ( 'NONE',  ( 0.000000000000000000, 0.000000000000000000, 0.000000000000000000 ) ) ;
#5615=ORIENTED_EDGE ( 'NONE', *, *, #6110, .F. ) ;
#5643=VECTOR ( 'NONE', #19695, 1000.000000000000000 ) ;
#5650=CIRCLE ( 'NONE', #1403, 4.000000000000000888 ) ;
#5652=EDGE_LOOP ( 'NONE', ( #15517, #21584, #17764, #3536 ) ) ;
#5662=DIRECTION ( 'NONE',  ( 1.000000000000000000, 0.000000000000000000, 0.000000000000000000 ) ) ;
#5675=CARTESIAN_POINT ( 'NONE',  ( 4.999999999999999112, -6.478011392632841314, -6.807171995660652897 ) ) ;
#5686=EDGE_CURVE ( 'NONE', #7993, #20599, #22245, .T. ) ;
#5703=AXIS2_PLACEMENT_3D ( 'NONE', #19409, #8659, #15959 ) ;
#5708=DIRECTION ( 'NONE',  ( 0.000000000000000000, 0.3090169943749411785, 0.9510565162951557516 ) ) ;
#5709=CIRCLE ( 'NONE', #8015, 11.00000000000000000 ) ;
#5729=CIRCLE ( 'NONE', #14163, 4.000000000000002665 ) ;
#5731=DIRECTION ( 'NONE',  ( 0.000000000000000000, 0.000000000000000000, 1.000000000000000000 ) ) ;
#5740=CIRCLE ( 'NONE', #4220, 4.000000000000001776 ) ;
#5751=DIRECTION ( 'NONE',  ( 0.000000000000000000, 0.8090169943749487835, -0.5877852522924714718 ) ) ;
#5756=VECTOR ( 'NONE', #23229, 1000.000000000000000 ) ;
#5759=VECTOR ( 'NONE', #17269, 1000.000000000000000 ) ;
#5760=CYLINDRICAL_SURFACE ( 'NONE', #3765, 8.749000000000002331 ) ;
#5761=EDGE_CURVE ( 'NONE', #21207, #12818, #19008, .T. ) ;
#5770=DIRECTION ( 'NONE',  ( -1.000000000000000000, 0.000000000000000000, 0.000000000000000000 ) ) ;
#5778=ORIENTED_EDGE ( 'NONE', *, *, #18444, .T. ) ;
#5788=AXIS2_PLACEMENT_3D ( 'NONE', #10800, #23210, #3106 ) ;
#5805=CARTESIAN_POINT ( 'NONE',  ( 4.999999999999999112, -1.699438267350438903, 9.241976615262153416 ) ) ;
#5808=DIRECTION ( 'NONE',  ( 0.000000000000000000, 0.000000000000000000, 1.000000000000000000 ) ) ;
#5811=DIRECTION ( 'NONE',  ( 0.000000000000000000, 0.000000000000000000, 1.000000000000000000 ) ) ;
#5812=DIRECTION ( 'NONE',  ( -1.000000000000000000, -0.000000000000000000, 0.000000000000000000 ) ) ;
#5816=DIRECTION ( 'NONE',  ( 0.000000000000000000, -0.5877852522924802425, 0.8090169943749422332 ) ) ;
#5824=ORIENTED_EDGE ( 'NONE', *, *, #21761, .T. ) ;
#5829=ORIENTED_EDGE ( 'NONE', *, *, #16449, .T. ) ;
#5851=CYLINDRICAL_SURFACE ( 'NONE', #16176, 11.00000000000000000 ) ;
#5853=ORIENTED_EDGE ( 'NONE', *, *, #6567, .T. ) ;
#5865=EDGE_CURVE ( 'NONE', #21100, #2825, #2602, .T. ) ;
#5867=EDGE_CURVE ( 'NONE', #2957, #11847, #4529, .T. ) ;
#5872=ORIENTED_EDGE ( 'NONE', *, *, #15308, .F. ) ;
#5873=VECTOR ( 'NONE', #5382, 1000.000000000000000 ) ;
#5879=CARTESIAN_POINT ( 'NONE',  ( -10.00000000000000000, 0.000000000000000000, 0.000000000000000000 ) ) ;
#5884=DIRECTION ( 'NONE',  ( -1.000000000000000000, 0.000000000000000000, 0.000000000000000000 ) ) ;
#5912=ORIENTED_EDGE ( 'NONE', *, *, #13607, .F. ) ;
#5925=DIRECTION ( 'NONE',  ( 0.000000000000000000, 0.9510565162951544194, -0.3090169943749446202 ) ) ;
#5926=VERTEX_POINT ( 'NONE', #4409 ) ;
#5930=CARTESIAN_POINT ( 'NONE',  ( 0.000000000000000000, -0.4999240074893842034, -8.734705317681632053 ) ) ;
#5946=APPLICATION_CONTEXT ( 'automotive_design' ) ;
#5947=VERTEX_POINT ( 'NONE', #8500 ) ;
#5948=CARTESIAN_POINT ( 'NONE',  ( 4.999999999999999112, 0.000000000000000000, 0.000000000000000000 ) ) ;
#5963=CARTESIAN_POINT ( 'NONE',  ( 0.000000000000000000, 7.360373001730918574, 4.729683950898897038 ) ) ;
#5969=CARTESIAN_POINT ( 'NONE',  ( 4.999999999999999112, 9.680994141368847394, -5.222868219166749704 ) ) ;
#5978=EDGE_LOOP ( 'NONE', ( #23320, #22301, #15007, #4560 ) ) ;
#6002=ADVANCED_FACE ( 'NONE', ( #19714 ), #18169, .T. ) ;
#6006=VECTOR ( 'NONE', #14444, 1000.000000000000000 ) ;
#6011=DIRECTION ( 'NONE',  ( -1.000000000000000000, 0.000000000000000000, 0.000000000000000000 ) ) ;
#6013=ORIENTED_EDGE ( 'NONE', *, *, #13779, .F. ) ;
#6021=CARTESIAN_POINT ( 'NONE',  ( 0.000000000000000000, 4.762163868918413812, -9.915734732513168836 ) ) ;
#6023=CYLINDRICAL_SURFACE ( 'NONE', #20764, 4.000000000000001776 ) ;
#6029=VECTOR ( 'NONE', #18872, 1000.000000000000000 ) ;
#6041=DIRECTION ( 'NONE',  ( -1.000000000000000000, -0.000000000000000000, 0.000000000000000000 ) ) ;
#6046=AXIS2_PLACEMENT_3D ( 'NONE', #10281, #23293, #23055 ) ;
#6047=CIRCLE ( 'NONE', #23246, 8.749000000000002331 ) ;
#6051=DIRECTION ( 'NONE',  ( -1.000000000000000000, -0.000000000000000000, -0.000000000000000000 ) ) ;
#6055=EDGE_CURVE ( 'NONE', #3223, #22912, #1425, .T. ) ;
#6070=AXIS2_PLACEMENT_3D ( 'NONE', #8078, #22890, #8430 ) ;
#6090=ORIENTED_EDGE ( 'NONE', *, *, #9929, .F. ) ;
#6092=LINE ( 'NONE', #15218, #18542 ) ;
#6094=CARTESIAN_POINT ( 'NONE',  ( 0.000000000000000000, 0.000000000000000000, 0.000000000000000000 ) ) ;
#6107=CARTESIAN_POINT ( 'NONE',  ( 0.000000000000000000, 0.000000000000000000, 0.000000000000000000 ) ) ;
#6110=EDGE_CURVE ( 'NONE', #16229, #9984, #18261, .T. ) ;
#6111=ORIENTED_EDGE ( 'NONE', *, *, #9687, .F. ) ;
#6113=CARTESIAN_POINT ( 'NONE',  ( 0.000000000000000000, 0.000000000000000000, 0.000000000000000000 ) ) ;
#6118=CARTESIAN_POINT ( 'NONE',  ( 0.000000000000000000, 0.000000000000000000, 0.000000000000000000 ) ) ;
#6138=EDGE_CURVE ( 'NONE', #16102, #22841, #12168, .T. ) ;
#6148=DIRECTION ( 'NONE',  ( -1.000000000000000000, -0.000000000000000000, -0.000000000000000000 ) ) ;
#6155=CIRCLE ( 'NONE', #3716, 8.749000000000004107 ) ;
#6158=ORIENTED_EDGE ( 'NONE', *, *, #1321, .T. ) ;
#6162=ADVANCED_FACE ( 'NONE', ( #1752 ), #21625, .T. ) ;
#6167=EDGE_CURVE ( 'NONE', #3575, #20722, #16733, .T. ) ;
#6174=EDGE_CURVE ( 'NONE', #4148, #8748, #5650, .T. ) ;
#6179=DIRECTION ( 'NONE',  ( 0.000000000000000000, -0.5877852522924802425, 0.8090169943749422332 ) ) ;
#6187=DIRECTION ( 'NONE',  ( 1.000000000000000000, -0.000000000000000000, 0.000000000000000000 ) ) ;
#6191=ORIENTED_EDGE ( 'NONE', *, *, #19908, .F. ) ;
#6192=DIRECTION ( 'NONE',  ( -1.000000000000000000, 0.000000000000000000, 0.000000000000000000 ) ) ;
#6196=CARTESIAN_POINT ( 'NONE',  ( 4.999999999999999112, -4.729683950898817102, -7.360373001730970977 ) ) ;
#6200=EDGE_CURVE ( 'NONE', #20722, #3223, #9879, .T. ) ;
#6208=DIRECTION ( 'NONE',  ( -1.000000000000000000, 0.000000000000000000, 0.000000000000000000 ) ) ;
#6212=CARTESIAN_POINT ( 'NONE',  ( 4.999999999999999112, -1.239665997526817165, -9.314797388894906049 ) ) ;
#6219=EDGE_LOOP ( 'NONE', ( #2871, #15284, #6438, #909 ) ) ;
#6225=DIRECTION ( 'NONE',  ( -1.000000000000000000, 0.000000000000000000, -0.000000000000000000 ) ) ;
#6229=ORIENTED_EDGE ( 'NONE', *, *, #8109, .F. ) ;
#6239=LINE ( 'NONE', #835, #10955 ) ;
#6250=ORIENTED_EDGE ( 'NONE', *, *, #8109, .T. ) ;
#6253=CARTESIAN_POINT ( 'NONE',  ( 0.000000000000000000, 7.958834565716766285, 7.593217523260609170 ) ) ;
#6269=DIRECTION ( 'NONE',  ( -1.000000000000000000, 0.000000000000000000, -0.000000000000000000 ) ) ;
#6284=ORIENTED_EDGE ( 'NONE', *, *, #11791, .F. ) ;
#6288=DIRECTION ( 'NONE',  ( 0.000000000000000000, 0.8090169943749487835, -0.5877852522924714718 ) ) ;
#6290=AXIS2_PLACEMENT_3D ( 'NONE', #20965, #19188, #19410 ) ;
#6291=DIRECTION ( 'NONE',  ( 0.000000000000000000, 0.000000000000000000, 1.000000000000000000 ) ) ;
#6305=VECTOR ( 'NONE', #21470, 1000.000000000000000 ) ;
#6310=EDGE_CURVE ( 'NONE', #2142, #9984, #20910, .T. ) ;
#6311=VERTEX_POINT ( 'NONE', #16611 ) ;
#6312=CARTESIAN_POINT ( 'NONE',  ( 4.999999999999999112, 9.241976615262160522, 2.300561732649595736 ) ) ;
#6321=ORIENTED_EDGE ( 'NONE', *, *, #6055, .T. ) ;
#6327=CYLINDRICAL_SURFACE ( 'NONE', #10570, 11.00000000000000000 ) ;
#6331=EDGE_CURVE ( 'NONE', #11486, #1543, #6412, .T. ) ;
#6340=CIRCLE ( 'NONE', #21608, 4.000000000000002665 ) ;
#6342=ORIENTED_EDGE ( 'NONE', *, *, #18614, .F. ) ;
#6355=CARTESIAN_POINT ( 'NONE',  ( 4.999999999999999112, 8.264486777890107660, 4.472189673936815879 ) ) ;
#6366=ORIENTED_EDGE ( 'NONE', *, *, #5865, .F. ) ;
#6395=CARTESIAN_POINT ( 'NONE',  ( 0.000000000000000000, -7.958834565716711218, -7.593217523260672230 ) ) ;
#6402=EDGE_CURVE ( 'NONE', #1668, #14298, #11720, .T. ) ;
#6412=CIRCLE ( 'NONE', #266, 11.00000000000000000 ) ;
#6421=DIRECTION ( 'NONE',  ( -1.000000000000000000, -0.000000000000000000, 0.000000000000000000 ) ) ;
#6423=DIRECTION ( 'NONE',  ( -1.000000000000000000, 0.000000000000000000, 0.000000000000000000 ) ) ;
#6427=CIRCLE ( 'NONE', #4512, 11.00000000000000000 ) ;
#6432=CIRCLE ( 'NONE', #7584, 4.000000000000001776 ) ;
#6437=ADVANCED_FACE ( 'NONE', ( #17088 ), #11838, .T. ) ;
#6438=ORIENTED_EDGE ( 'NONE', *, *, #18002, .T. ) ;
#6440=AXIS2_PLACEMENT_3D ( 'NONE', #2732, #15351, #4768 ) ;
#6441=CARTESIAN_POINT ( 'NONE',  ( 0.000000000000000000, 5.222868219166995729, -9.680994141368717720 ) ) ;
#6445=FACE_OUTER_BOUND ( 'NONE', #16678, .T. ) ;
#6456=DIRECTION ( 'NONE',  ( -1.000000000000000000, 0.000000000000000000, -0.000000000000000000 ) ) ;
#6468=DIRECTION ( 'NONE',  ( -1.000000000000000000, 0.000000000000000000, 0.000000000000000000 ) ) ;
#6473=DIRECTION ( 'NONE',  ( 0.000000000000000000, 0.000000000000000000, 1.000000000000000000 ) ) ;
#6478=AXIS2_PLACEMENT_3D ( 'NONE', #4193, #17015, #4776 ) ;
#6491=ORIENTED_EDGE ( 'NONE', *, *, #1593, .F. ) ;
#6501=EDGE_CURVE ( 'NONE', #11365, #11624, #17130, .T. ) ;
#6505=CARTESIAN_POINT ( 'NONE',  ( -10.00000000000000000, 0.000000000000000000, 0.000000000000000000 ) ) ;
#6515=VERTEX_POINT ( 'NONE', #12675 ) ;
#6517=VERTEX_POINT ( 'NONE', #8701 ) ;
#6522=CARTESIAN_POINT ( 'NONE',  ( 5.000000000000000888, 0.000000000000000000, 0.000000000000000000 ) ) ;
#6534=AXIS2_PLACEMENT_3D ( 'NONE', #18908, #7442, #351 ) ;
#6542=CARTESIAN_POINT ( 'NONE',  ( -10.00000000000000000, 0.000000000000000000, 0.000000000000000000 ) ) ;
#6545=ORIENTED_EDGE ( 'NONE', *, *, #16954, .F. ) ;
#6547=DIRECTION ( 'NONE',  ( -1.000000000000000000, 0.000000000000000000, 0.000000000000000000 ) ) ;
#6566=CARTESIAN_POINT ( 'NONE',  ( 5.000000000000000888, 0.000000000000000000, 4.000000000000000000 ) ) ;
#6567=EDGE_CURVE ( 'NONE', #11236, #5065, #6432, .T. ) ;
#6574=VERTEX_POINT ( 'NONE', #12310 ) ;
#6585=CARTESIAN_POINT ( 'NONE',  ( 4.999999999999999112, -9.314797388894900720, 1.239665997526853580 ) ) ;
#6589=EDGE_CURVE ( 'NONE', #2537, #18556, #9500, .T. ) ;
#6599=CARTESIAN_POINT ( 'NONE',  ( 0.000000000000000000, 10.82112760146736363, 1.975651141462276161 ) ) ;
#6607=ORIENTED_EDGE ( 'NONE', *, *, #2874, .F. ) ;
#6622=DIRECTION ( 'NONE',  ( -1.000000000000000000, -0.000000000000000000, -0.000000000000000000 ) ) ;
#6632=ADVANCED_FACE ( 'NONE', ( #16474 ), #11215, .T. ) ;
#6639=ORIENTED_EDGE ( 'NONE', *, *, #17117, .T. ) ;
#6649=CYLINDRICAL_SURFACE ( 'NONE', #13532, 8.749000000000002331 ) ;
#6651=DIRECTION ( 'NONE',  ( -1.000000000000000000, 0.000000000000000000, -0.000000000000000000 ) ) ;
#6655=DIRECTION ( 'NONE',  ( 0.000000000000000000, 0.3090169943749481174, -0.9510565162951533091 ) ) ;
#6659=DIRECTION ( 'NONE',  ( -1.000000000000000000, 0.000000000000000000, 0.000000000000000000 ) ) ;
#6665=VERTEX_POINT ( 'NONE', #165 ) ;
#6669=ORIENTED_EDGE ( 'NONE', *, *, #11696, .F. ) ;
#6674=FACE_OUTER_BOUND ( 'NONE', #1274, .T. ) ;
#6683=LINE ( 'NONE', #21502, #17454 ) ;
#6687=ORIENTED_EDGE ( 'NONE', *, *, #845, .F. ) ;
#6689=EDGE_LOOP ( 'NONE', ( #492, #21529, #7532, #21356 ) ) ;
#6697=CARTESIAN_POINT ( 'NONE',  ( 2.499999999999999556, -9.915734732513184824, -4.762163868918378284 ) ) ;
#6699=ORIENTED_EDGE ( 'NONE', *, *, #11564, .F. ) ;
#6706=CARTESIAN_POINT ( 'NONE',  ( 2.499999999999999556, 1.975651141462237970, 10.82112760146736896 ) ) ;
#6709=DIRECTION ( 'NONE',  ( -1.000000000000000000, -0.000000000000000000, -0.000000000000000000 ) ) ;
#6720=ORIENTED_EDGE ( 'NONE', *, *, #5761, .T. ) ;
#6735=EDGE_CURVE ( 'NONE', #16674, #2643, #1056, .T. ) ;
#6736=AXIS2_PLACEMENT_3D ( 'NONE', #17591, #10303, #8496 ) ;
#6749=ORIENTED_EDGE ( 'NONE', *, *, #13786, .F. ) ;
#6751=ORIENTED_EDGE ( 'NONE', *, *, #13943, .F. ) ;
#6753=VERTEX_POINT ( 'NONE', #18734 ) ;
#6756=ADVANCED_FACE ( 'NONE', ( #2323 ), #16586, .T. ) ;
#6795=LINE ( 'NONE', #14473, #22001 ) ;
#6801=AXIS2_PLACEMENT_3D ( 'NONE', #10783, #17598, #21507 ) ;
#6806=ORIENTED_EDGE ( 'NONE', *, *, #16256, .T. ) ;
#6811=AXIS2_PLACEMENT_3D ( 'NONE', #12230, #6468, #8272 ) ;
#6818=CYLINDRICAL_SURFACE ( 'NONE', #8788, 4.000000000000000888 ) ;
#6822=VERTEX_POINT ( 'NONE', #4598 ) ;
#6833=DIRECTION ( 'NONE',  ( 0.000000000000000000, 0.000000000000000000, 1.000000000000000000 ) ) ;
#6834=ORIENTED_EDGE ( 'NONE', *, *, #15797, .T. ) ;
#6836=VECTOR ( 'NONE', #9125, 1000.000000000000000 ) ;
#6865=ORIENTED_EDGE ( 'NONE', *, *, #16227, .F. ) ;
#6873=PRODUCT_DEFINITION_FORMATION_WITH_SPECIFIED_SOURCE ( 'ANY', '', #11248, .NOT_KNOWN. ) ;
#6883=CIRCLE ( 'NONE', #20250, 4.000000000000001776 ) ;
#6885=EDGE_CURVE ( 'NONE', #10460, #2926, #20750, .T. ) ;
#6888=LINE ( 'NONE', #10852, #16064 ) ;
#6892=LINE ( 'NONE', #12540, #21960 ) ;
#6893=EDGE_LOOP ( 'NONE', ( #13893, #215, #13707, #15917 ) ) ;
#6897=EDGE_CURVE ( 'NONE', #2984, #3455, #22788, .T. ) ;
#6899=VERTEX_POINT ( 'NONE', #6395 ) ;
#6914=CARTESIAN_POINT ( 'NONE',  ( 4.999999999999999112, 0.000000000000000000, 0.000000000000000000 ) ) ;
#6921=CARTESIAN_POINT ( 'NONE',  ( 0.000000000000000000, 0.000000000000000000, 0.000000000000000000 ) ) ;
#6922=DIRECTION ( 'NONE',  ( 0.000000000000000000, 0.000000000000000000, 1.000000000000000000 ) ) ;
#6929=CARTESIAN_POINT ( 'NONE',  ( 0.000000000000000000, 0.000000000000000000, 0.000000000000000000 ) ) ;
#6930=DIRECTION ( 'NONE',  ( -1.000000000000000000, 0.000000000000000000, 0.000000000000000000 ) ) ;
#6931=EDGE_CURVE ( 'NONE', #1543, #7617, #8371, .T. ) ;
#6933=EDGE_CURVE ( 'NONE', #15752, #21976, #6047, .T. ) ;
#6934=DIRECTION ( 'NONE',  ( -1.000000000000000000, -0.000000000000000000, -0.000000000000000000 ) ) ;
#6937=ORIENTED_EDGE ( 'NONE', *, *, #2903, .F. ) ;
#6959=DIRECTION ( 'NONE',  ( 0.000000000000000000, -1.000000000000000000, -0.000000000000000000 ) ) ;
#6964=ORIENTED_EDGE ( 'NONE', *, *, #13185, .T. ) ;
#6966=DIRECTION ( 'NONE',  ( 0.000000000000000000, 0.000000000000000000, 1.000000000000000000 ) ) ;
#7004=CIRCLE ( 'NONE', #8935, 11.00000000000000000 ) ;
#7032=CARTESIAN_POINT ( 'NONE',  ( 0.000000000000000000, 0.000000000000000000, 0.000000000000000000 ) ) ;
#7041=CYLINDRICAL_SURFACE ( 'NONE', #1914, 6.000000000000000888 ) ;
#7042=DIRECTION ( 'NONE',  ( -1.000000000000000000, 0.000000000000000000, 0.000000000000000000 ) ) ;
#7048=VERTEX_POINT ( 'NONE', #21326 ) ;
#7054=CARTESIAN_POINT ( 'NONE',  ( 0.000000000000000000, 9.314797388894909602, -1.239665997526783858 ) ) ;
#7057=LINE ( 'NONE', #14376, #4552 ) ;
#7086=SURFACE_SIDE_STYLE ('',( #12964 ) ) ;
#7087=CARTESIAN_POINT ( 'NONE',  ( 4.999999999999999112, 4.472189673936902921, -8.264486777890061475 ) ) ;
#7093=EDGE_CURVE ( 'NONE', #11644, #17824, #19796, .T. ) ;
#7098=DIRECTION ( 'NONE',  ( -1.000000000000000000, 0.000000000000000000, 0.000000000000000000 ) ) ;
#7117=AXIS2_PLACEMENT_3D ( 'NONE', #6094, #9948, #22613 ) ;
#7128=DIRECTION ( 'NONE',  ( -1.000000000000000000, 0.000000000000000000, -0.000000000000000000 ) ) ;
#7130=CARTESIAN_POINT ( 'NONE',  ( 4.999999999999999112, 8.152713396088763886, 3.174628368996105010 ) ) ;
#7132=ORIENTED_EDGE ( 'NONE', *, *, #22666, .T. ) ;
#7144=CARTESIAN_POINT ( 'NONE',  ( 4.999999999999999112, 8.264486777890107660, 4.472189673936815879 ) ) ;
#7162=ORIENTED_EDGE ( 'NONE', *, *, #12594, .F. ) ;
#7163=ORIENTED_EDGE ( 'NONE', *, *, #19059, .T. ) ;
#7174=ADVANCED_FACE ( 'NONE', ( #14426 ), #18001, .T. ) ;
#7192=EDGE_LOOP ( 'NONE', ( #10329, #23299, #13982, #13401 ) ) ;
#7196=FACE_OUTER_BOUND ( 'NONE', #2731, .T. ) ;
#7198=ORIENTED_EDGE ( 'NONE', *, *, #20433, .T. ) ;
#7199=CARTESIAN_POINT ( 'NONE',  ( 0.000000000000000000, -8.461683424509331530, 2.223716399045538861 ) ) ;
#7201=PLANE ( 'NONE',  #8613 ) ;
#7203=ORIENTED_EDGE ( 'NONE', *, *, #16552, .T. ) ;
#7216=CARTESIAN_POINT ( 'NONE',  ( 4.999999999999999112, -1.975651141462163363, -10.82112760146738495 ) ) ;
#7218=CARTESIAN_POINT ( 'NONE',  ( 4.999999999999999112, 8.152713396088806519, -3.174628368995992655 ) ) ;
#7234=EDGE_LOOP ( 'NONE', ( #9009, #13187, #22087, #14250 ) ) ;
#7247=DIRECTION ( 'NONE',  ( 0.000000000000000000, 0.000000000000000000, 1.000000000000000000 ) ) ;
#7250=AXIS2_PLACEMENT_3D ( 'NONE', #12352, #19614, #10559 ) ;
#7255=DIRECTION ( 'NONE',  ( -1.000000000000000000, -0.000000000000000000, -0.000000000000000000 ) ) ;
#7267=CARTESIAN_POINT ( 'NONE',  ( 4.999999999999999112, 6.807171995660675101, -6.478011392632816445 ) ) ;
#7275=PRODUCT_DEFINITION ( 'UNKNOWN', '', #6873, #22705 ) ;
#7293=AXIS2_PLACEMENT_3D ( 'NONE', #5406, #122, #16660 ) ;
#7299=ORIENTED_EDGE ( 'NONE', *, *, #1992, .F. ) ;
#7302=CIRCLE ( 'NONE', #9221, 4.000000000000001776 ) ;
#7314=CARTESIAN_POINT ( 'NONE',  ( 4.999999999999999112, 4.057423117305515525, -8.475820894092930047 ) ) ;
#7318=AXIS2_PLACEMENT_3D ( 'NONE', #3111, #10686, #17843 ) ;
#7344=CYLINDRICAL_SURFACE ( 'NONE', #7293, 8.749000000000002331 ) ;
#7372=ADVANCED_FACE ( 'NONE', ( #2728 ), #18902, .T. ) ;
#7385=DIRECTION ( 'NONE',  ( 0.000000000000000000, 0.000000000000000000, 1.000000000000000000 ) ) ;
#7392=CARTESIAN_POINT ( 'NONE',  ( 0.000000000000000000, 0.000000000000000000, 0.000000000000000000 ) ) ;
#7399=DIRECTION ( 'NONE',  ( 1.000000000000000000, 0.000000000000000000, -0.000000000000000000 ) ) ;
#7403=CYLINDRICAL_SURFACE ( 'NONE', #1842, 11.00000000000000000 ) ;
#7416=DIRECTION ( 'NONE',  ( 0.000000000000000000, 0.9510565162951521989, 0.3090169943749515591 ) ) ;
#7419=VERTEX_POINT ( 'NONE', #13429 ) ;
#7427=AXIS2_PLACEMENT_3D ( 'NONE', #7392, #7507, #5342 ) ;
#7431=CARTESIAN_POINT ( 'NONE',  ( 4.999999999999999112, -8.475820894093002877, 4.057423117305363647 ) ) ;
#7437=LINE ( 'NONE', #21783, #6836 ) ;
#7442=DIRECTION ( 'NONE',  ( -1.000000000000000000, -0.000000000000000000, -0.000000000000000000 ) ) ;
#7445=CARTESIAN_POINT ( 'NONE',  ( 0.000000000000000000, -2.223716399045629899, 8.461683424509306661 ) ) ;
#7452=DIRECTION ( 'NONE',  ( -1.000000000000000000, -0.000000000000000000, -0.000000000000000000 ) ) ;
#7453=AXIS2_PLACEMENT_3D ( 'NONE', #19923, #3285, #21710 ) ;
#7457=CARTESIAN_POINT ( 'NONE',  ( 4.999999999999999112, 9.314797388894893615, 1.239665997526919083 ) ) ;
#7466=EDGE_CURVE ( 'NONE', #3547, #12645, #12170, .T. ) ;
#7471=VECTOR ( 'NONE', #4704, 1000.000000000000000 ) ;
#7474=ADVANCED_FACE ( 'NONE', ( #12452 ), #1636, .T. ) ;
#7485=DIRECTION ( 'NONE',  ( -1.000000000000000000, 0.000000000000000000, 0.000000000000000000 ) ) ;
#7497=ADVANCED_FACE ( 'NONE', ( #16035 ), #22971, .T. ) ;
#7506=CIRCLE ( 'NONE', #19326, 4.000000000000001776 ) ;
#7507=DIRECTION ( 'NONE',  ( -1.000000000000000000, 0.000000000000000000, 0.000000000000000000 ) ) ;
#7515=ORIENTED_EDGE ( 'NONE', *, *, #3762, .F. ) ;
#7517=DIRECTION ( 'NONE',  ( -1.000000000000000000, 0.000000000000000000, 0.000000000000000000 ) ) ;
#7524=DIRECTION ( 'NONE',  ( 1.000000000000000000, -0.000000000000000000, -0.000000000000000000 ) ) ;
#7532=ORIENTED_EDGE ( 'NONE', *, *, #21343, .T. ) ;
#7540=ORIENTED_EDGE ( 'NONE', *, *, #18829, .T. ) ;
#7541=CARTESIAN_POINT ( 'NONE',  ( 2.499999999999999556, -1.464956435139468161, -10.90201369670500497 ) ) ;
#7543=DIRECTION ( 'NONE',  ( 0.000000000000000000, 0.000000000000000000, 1.000000000000000000 ) ) ;
#7548=DIRECTION ( 'NONE',  ( 0.000000000000000000, 0.000000000000000000, 1.000000000000000000 ) ) ;
#7549=ORIENTED_EDGE ( 'NONE', *, *, #6167, .F. ) ;
#7551=ORIENTED_EDGE ( 'NONE', *, *, #17410, .T. ) ;
#7553=VECTOR ( 'NONE', #7485, 1000.000000000000000 ) ;
#7564=CARTESIAN_POINT ( 'NONE',  ( 2.499999999999999556, 9.680994141368771011, 5.222868219166890036 ) ) ;
#7584=AXIS2_PLACEMENT_3D ( 'NONE', #3531, #5088, #3414 ) ;
#7595=CIRCLE ( 'NONE', #21722, 4.000000000000000888 ) ;
#7605=CARTESIAN_POINT ( 'NONE',  ( 0.000000000000000000, -9.314797388894900720, 1.239665997526853580 ) ) ;
#7617=VERTEX_POINT ( 'NONE', #15556 ) ;
#7620=DIRECTION ( 'NONE',  ( 0.000000000000000000, 0.8090169943749444537, 0.5877852522924770229 ) ) ;
#7625=AXIS2_PLACEMENT_3D ( 'NONE', #13725, #19092, #11586 ) ;
#7626=DIRECTION ( 'NONE',  ( 0.000000000000000000, 0.000000000000000000, 1.000000000000000000 ) ) ;
#7631=DIRECTION ( 'NONE',  ( -1.000000000000000000, 0.000000000000000000, 0.000000000000000000 ) ) ;
#7632=LINE ( 'NONE', #4136, #23140 ) ;
#7634=FACE_OUTER_BOUND ( 'NONE', #3971, .T. ) ;
#7638=DIRECTION ( 'NONE',  ( 0.000000000000000000, 0.000000000000000000, 1.000000000000000000 ) ) ;
#7649=ORIENTED_EDGE ( 'NONE', *, *, #12863, .F. ) ;
#7653=DIRECTION ( 'NONE',  ( -1.000000000000000000, 0.000000000000000000, 0.000000000000000000 ) ) ;
#7660=CIRCLE ( 'NONE', #14179, 11.00000000000000000 ) ;
#7662=AXIS2_PLACEMENT_3D ( 'NONE', #7032, #14705, #21961 ) ;
#7666=CARTESIAN_POINT ( 'NONE',  ( 4.999999999999999112, -0.4999240074893842034, -8.734705317681632053 ) ) ;
#7669=CYLINDRICAL_SURFACE ( 'NONE', #8959, 4.000000000000001776 ) ;
#7671=EDGE_CURVE ( 'NONE', #22394, #14554, #4147, .T. ) ;
#7692=AXIS2_PLACEMENT_3D ( 'NONE', #13679, #12008, #13806 ) ;
#7693=CARTESIAN_POINT ( 'NONE',  ( 4.999999999999999112, 9.241976615262160522, -1.699438267350405818 ) ) ;
#7697=CARTESIAN_POINT ( 'NONE',  ( 25.00005080000000035, 3.872983346207417021, -1.000000000000000000 ) ) ;
#7699=CYLINDRICAL_SURFACE ( 'NONE', #11221, 4.000000000000001776 ) ;
#7701=CARTESIAN_POINT ( 'NONE',  ( 4.999999999999999112, 0.000000000000000000, 0.000000000000000000 ) ) ;
#7710=VERTEX_POINT ( 'NONE', #22590 ) ;
#7721=DIRECTION ( 'NONE',  ( -1.000000000000000000, -0.000000000000000000, 0.000000000000000000 ) ) ;
#7737=DIRECTION ( 'NONE',  ( 0.000000000000000000, 0.000000000000000000, 1.000000000000000000 ) ) ;
#7738=CARTESIAN_POINT ( 'NONE',  ( 4.999999999999999112, -1.699438267350438903, 9.241976615262153416 ) ) ;
#7740=EDGE_CURVE ( 'NONE', #8014, #16322, #14877, .T. ) ;
#7745=EDGE_CURVE ( 'NONE', #22278, #20599, #10673, .T. ) ;
#7747=DIRECTION ( 'NONE',  ( 0.000000000000000000, 0.000000000000000000, -1.000000000000000000 ) ) ;
#7751=CARTESIAN_POINT ( 'NONE',  ( 4.999999999999999112, 0.000000000000000000, 0.000000000000000000 ) ) ;
#7761=VERTEX_POINT ( 'NONE', #19463 ) ;
#7768=DIRECTION ( 'NONE',  ( 1.000000000000000000, 0.000000000000000000, 0.000000000000000000 ) ) ;
#7776=CARTESIAN_POINT ( 'NONE',  ( 4.999999999999999112, -8.152713396088785203, 3.174628368996045946 ) ) ;
#7778=CARTESIAN_POINT ( 'NONE',  ( 25.00005080000000035, 5.400000000000000355, -1.000000000000000000 ) ) ;
#7788=CARTESIAN_POINT ( 'NONE',  ( 0.000000000000000000, 7.593217523260583413, 7.958834565716794707 ) ) ;
#7789=AXIS2_PLACEMENT_3D ( 'NONE', #970, #4227, #9871 ) ;
#7795=EDGE_CURVE ( 'NONE', #3403, #22760, #22880, .T. ) ;
#7804=DIRECTION ( 'NONE',  ( 0.000000000000000000, 0.3090169943749481174, -0.9510565162951533091 ) ) ;
#7807=CYLINDRICAL_SURFACE ( 'NONE', #19290, 11.00000000000000000 ) ;
#7842=ORIENTED_EDGE ( 'NONE', *, *, #7745, .F. ) ;
#7864=ORIENTED_EDGE ( 'NONE', *, *, #3766, .F. ) ;
#7869=ORIENTED_EDGE ( 'NONE', *, *, #15276, .F. ) ;
#7871=EDGE_CURVE ( 'NONE', #14298, #2537, #9897, .T. ) ;
#7874=CARTESIAN_POINT ( 'NONE',  ( 4.999999999999999112, -5.222868219166784343, -9.680994141368826078 ) ) ;
#7889=EDGE_CURVE ( 'NONE', #15752, #2469, #678, .T. ) ;
#7934=ADVANCED_FACE ( 'NONE', ( #22062 ), #12784, .T. ) ;
#7957=ORIENTED_EDGE ( 'NONE', *, *, #11701, .F. ) ;
#7958=DIRECTION ( 'NONE',  ( 0.000000000000000000, 0.000000000000000000, 1.000000000000000000 ) ) ;
#7959=ORIENTED_EDGE ( 'NONE', *, *, #23411, .T. ) ;
#7969=CIRCLE ( 'NONE', #19424, 4.000000000000001776 ) ;
#7972=CIRCLE ( 'NONE', #17146, 6.000000000000000888 ) ;
#7981=DIRECTION ( 'NONE',  ( 0.000000000000000000, 0.000000000000000000, -1.000000000000000000 ) ) ;
#7993=VERTEX_POINT ( 'NONE', #16705 ) ;
#7998=ORIENTED_EDGE ( 'NONE', *, *, #9997, .T. ) ;
#8003=ADVANCED_FACE ( 'NONE', ( #12893 ), #20150, .T. ) ;
#8006=ORIENTED_EDGE ( 'NONE', *, *, #7466, .T. ) ;
#8007=CARTESIAN_POINT ( 'NONE',  ( 4.999999999999999112, 9.241976615262160522, -1.699438267350405818 ) ) ;
#8008=CIRCLE ( 'NONE', #1858, 4.000000000000001776 ) ;
#8014=VERTEX_POINT ( 'NONE', #166 ) ;
#8015=AXIS2_PLACEMENT_3D ( 'NONE', #19715, #12097, #14001 ) ;
#8016=LINE ( 'NONE', #4404, #19882 ) ;
#8020=VECTOR ( 'NONE', #11884, 1000.000000000000000 ) ;
#8024=DIRECTION ( 'NONE',  ( 0.000000000000000000, 0.000000000000000000, 1.000000000000000000 ) ) ;
#8031=CARTESIAN_POINT ( 'NONE',  ( 4.999999999999999112, 4.762163868918272591, 9.915734732513236338 ) ) ;
#8055=DIRECTION ( 'NONE',  ( 0.000000000000000000, 0.3090169943749411785, 0.9510565162951557516 ) ) ;
#8072=ADVANCED_FACE ( 'NONE', ( #20515 ), #2324, .T. ) ;
#8078=CARTESIAN_POINT ( 'NONE',  ( 4.999999999999999112, -9.241976615262169403, 1.699438267350339871 ) ) ;
#8081=CARTESIAN_POINT ( 'NONE',  ( 0.000000000000000000, -9.241976615262146311, -1.699438267350473097 ) ) ;
#8109=EDGE_CURVE ( 'NONE', #22760, #2984, #4897, .T. ) ;
#8133=DIRECTION ( 'NONE',  ( -1.000000000000000000, 0.000000000000000000, 0.000000000000000000 ) ) ;
#8137=DIRECTION ( 'NONE',  ( -1.000000000000000000, 0.000000000000000000, 0.000000000000000000 ) ) ;
#8138=FACE_OUTER_BOUND ( 'NONE', #22549, .T. ) ;
#8147=AXIS2_PLACEMENT_3D ( 'NONE', #810, #22720, #20800 ) ;
#8167=DIRECTION ( 'NONE',  ( -1.000000000000000000, -0.000000000000000000, 0.000000000000000000 ) ) ;
#8177=ORIENTED_EDGE ( 'NONE', *, *, #12594, .T. ) ;
#8178=ORIENTED_EDGE ( 'NONE', *, *, #11158, .T. ) ;
#8182=CIRCLE ( 'NONE', #16210, 8.749000000000000554 ) ;
#8184=VECTOR ( 'NONE', #17268, 1000.000000000000000 ) ;
#8189=DIRECTION ( 'NONE',  ( 0.000000000000000000, 0.000000000000000000, -1.000000000000000000 ) ) ;
#8192=CARTESIAN_POINT ( 'NONE',  ( 0.000000000000000000, 0.000000000000000000, 0.000000000000000000 ) ) ;
#8195=EDGE_LOOP ( 'NONE', ( #8307, #7299, #3217, #11695 ) ) ;
#8197=LINE ( 'NONE', #2666, #7471 ) ;
#8205=ORIENTED_EDGE ( 'NONE', *, *, #5101, .T. ) ;
#8215=FACE_OUTER_BOUND ( 'NONE', #1609, .T. ) ;
#8226=CARTESIAN_POINT ( 'NONE',  ( 4.999999999999999112, 6.478011392632982535, -6.807171995660517005 ) ) ;
#8227=EDGE_LOOP ( 'NONE', ( #20489, #17327, #22883, #5778 ) ) ;
#8232=AXIS2_PLACEMENT_3D ( 'NONE', #22745, #4432, #9616 ) ;
#8238=EDGE_CURVE ( 'NONE', #990, #11486, #4518, .T. ) ;
#8240=EDGE_CURVE ( 'NONE', #16346, #19924, #7595, .T. ) ;
#8249=CARTESIAN_POINT ( 'NONE',  ( 4.999999999999999112, 0.4999240074895661690, -8.734705317681621395 ) ) ;
#8255=LINE ( 'NONE', #919, #10452 ) ;
#8259=DIRECTION ( 'NONE',  ( -1.000000000000000000, -0.000000000000000000, -0.000000000000000000 ) ) ;
#8272=DIRECTION ( 'NONE',  ( 0.000000000000000000, -0.9510565162951565288, 0.3090169943749382364 ) ) ;
#8280=DIRECTION ( 'NONE',  ( 0.000000000000000000, 0.5877852522924684742, 0.8090169943749507819 ) ) ;
#8284=DIRECTION ( 'NONE',  ( 0.000000000000000000, 0.000000000000000000, 1.000000000000000000 ) ) ;
#8285=DIRECTION ( 'NONE',  ( -1.000000000000000000, 0.000000000000000000, 0.000000000000000000 ) ) ;
#8307=ORIENTED_EDGE ( 'NONE', *, *, #21132, .T. ) ;
#8308=FACE_OUTER_BOUND ( 'NONE', #5019, .T. ) ;
#8312=EDGE_LOOP ( 'NONE', ( #8940, #9060, #13065, #20311 ) ) ;
#8313=AXIS2_PLACEMENT_3D ( 'NONE', #16074, #23363, #2876 ) ;
#8314=DIRECTION ( 'NONE',  ( -1.000000000000000000, 0.000000000000000000, 0.000000000000000000 ) ) ;
#8341=LINE ( 'NONE', #19332, #1653 ) ;
#8348=VERTEX_POINT ( 'NONE', #1457 ) ;
#8362=CIRCLE ( 'NONE', #17540, 4.000000000000001776 ) ;
#8363=CARTESIAN_POINT ( 'NONE',  ( 4.999999999999999112, 0.000000000000000000, 0.000000000000000000 ) ) ;
#8370=EDGE_CURVE ( 'NONE', #20722, #19770, #8558, .T. ) ;
#8371=CIRCLE ( 'NONE', #308, 4.000000000000001776 ) ;
#8374=DIRECTION ( 'NONE',  ( -1.000000000000000000, 0.000000000000000000, 0.000000000000000000 ) ) ;
#8386=DIRECTION ( 'NONE',  ( -1.000000000000000000, 0.000000000000000000, 0.000000000000000000 ) ) ;
#8408=DIRECTION ( 'NONE',  ( -1.000000000000000000, -0.000000000000000000, -0.000000000000000000 ) ) ;
#8411=ORIENTED_EDGE ( 'NONE', *, *, #4401, .F. ) ;
#8430=DIRECTION ( 'NONE',  ( 0.000000000000000000, -0.3090169943749551673, 0.9510565162951511997 ) ) ;
#8442=ORIENTED_EDGE ( 'NONE', *, *, #13905, .T. ) ;
#8449=EDGE_CURVE ( 'NONE', #6753, #4288, #3705, .T. ) ;
#8450=AXIS2_PLACEMENT_3D ( 'NONE', #7457, #5520, #126 ) ;
#8472=LINE ( 'NONE', #17445, #930 ) ;
#8476=EDGE_LOOP ( 'NONE', ( #3116, #6720, #10215, #2867 ) ) ;
#8481=ORIENTED_EDGE ( 'NONE', *, *, #13199, .F. ) ;
#8494=ORIENTED_EDGE ( 'NONE', *, *, #17769, .F. ) ;
#8496=DIRECTION ( 'NONE',  ( -1.000000000000000000, 0.000000000000000000, -0.000000000000000000 ) ) ;
#8497=CARTESIAN_POINT ( 'NONE',  ( 4.999999999999999112, 2.223716399045570835, 8.461683424509324425 ) ) ;
#8500=CARTESIAN_POINT ( 'NONE',  ( 0.000000000000000000, -8.152713396088785203, 3.174628368996045946 ) ) ;
#8503=DIRECTION ( 'NONE',  ( -1.000000000000000000, 0.000000000000000000, -0.000000000000000000 ) ) ;
#8506=ORIENTED_EDGE ( 'NONE', *, *, #17253, .F. ) ;
#8512=LINE ( 'NONE', #6697, #14850 ) ;
#8520=ORIENTED_EDGE ( 'NONE', *, *, #16413, .T. ) ;
#8538=CARTESIAN_POINT ( 'NONE',  ( 0.000000000000000000, 0.000000000000000000, 0.000000000000000000 ) ) ;
#8550=EDGE_LOOP ( 'NONE', ( #11533, #1709, #7959, #18276 ) ) ;
#8556=CIRCLE ( 'NONE', #17340, 8.749000000000002331 ) ;
#8558=LINE ( 'NONE', #13843, #23209 ) ;
#8568=CARTESIAN_POINT ( 'NONE',  ( 4.999999999999999112, 9.241976615262160522, 2.300561732649595736 ) ) ;
#8569=VECTOR ( 'NONE', #12793, 1000.000000000000000 ) ;
#8590=CARTESIAN_POINT ( 'NONE',  ( 0.000000000000000000, -6.807171995660539210, -6.478011392632959442 ) ) ;
#8592=DIRECTION ( 'NONE',  ( -1.000000000000000000, 0.000000000000000000, 0.000000000000000000 ) ) ;
#8599=DIRECTION ( 'NONE',  ( -1.000000000000000000, -0.000000000000000000, -0.000000000000000000 ) ) ;
#8612=ORIENTED_EDGE ( 'NONE', *, *, #252, .F. ) ;
#8613=AXIS2_PLACEMENT_3D ( 'NONE', #10455, #6959, #17965 ) ;
#8615=AXIS2_PLACEMENT_3D ( 'NONE', #16345, #7255, #10507 ) ;
#8620=ORIENTED_EDGE ( 'NONE', *, *, #16954, .T. ) ;
#8634=CARTESIAN_POINT ( 'NONE',  ( 0.000000000000000000, -1.975651141462162474, -10.82112760146738673 ) ) ;
#8659=DIRECTION ( 'NONE',  ( -1.000000000000000000, 0.000000000000000000, -0.000000000000000000 ) ) ;
#8660=CARTESIAN_POINT ( 'NONE',  ( 0.000000000000000000, 9.915734732513284300, -4.762163868918174892 ) ) ;
#8663=EDGE_CURVE ( 'NONE', #17247, #12645, #9864, .T. ) ;
#8685=CARTESIAN_POINT ( 'NONE',  ( 4.999999999999999112, 6.772677083992466152, -5.538577986808826736 ) ) ;
#8690=CARTESIAN_POINT ( 'NONE',  ( 4.999999999999999112, 0.000000000000000000, 0.000000000000000000 ) ) ;
#8699=ORIENTED_EDGE ( 'NONE', *, *, #310, .F. ) ;
#8700=ORIENTED_EDGE ( 'NONE', *, *, #19710, .F. ) ;
#8701=CARTESIAN_POINT ( 'NONE',  ( 4.999999999999999112, 9.915734732513284300, -4.762163868918172227 ) ) ;
#8703=DIRECTION ( 'NONE',  ( 1.000000000000000000, 0.000000000000000000, 0.000000000000000000 ) ) ;
#8708=AXIS2_PLACEMENT_3D ( 'NONE', #22124, #13071, #20327 ) ;
#8711=DIRECTION ( 'NONE',  ( 0.000000000000000000, 0.000000000000000000, 1.000000000000000000 ) ) ;
#8717=DIRECTION ( 'NONE',  ( 0.000000000000000000, 0.000000000000000000, 1.000000000000000000 ) ) ;
#8718=ORIENTED_EDGE ( 'NONE', *, *, #19021, .T. ) ;
#8720=DIRECTION ( 'NONE',  ( 0.000000000000000000, 0.000000000000000000, 1.000000000000000000 ) ) ;
#8721=CARTESIAN_POINT ( 'NONE',  ( -20.00005080000000035, 0.000000000000000000, 0.000000000000000000 ) ) ;
#8728=VERTEX_POINT ( 'NONE', #20154 ) ;
#8731=ADVANCED_FACE ( 'NONE', ( #9068 ), #14458, .T. ) ;
#8734=CIRCLE ( 'NONE', #670, 6.000000000000000888 ) ;
#8736=CARTESIAN_POINT ( 'NONE',  ( 2.499999999999999556, 10.90201369670498721, -1.464956435139581403 ) ) ;
#8742=( GEOMETRIC_REPRESENTATION_CONTEXT ( 3 ) GLOBAL_UNCERTAINTY_ASSIGNED_CONTEXT ( ( #4030 ) ) GLOBAL_UNIT_ASSIGNED_CONTEXT ( ( #9057, #5441, #20143 ) ) REPRESENTATION_CONTEXT ( 'NONE', 'WORKASPACE' ) );
#8743=DIRECTION ( 'NONE',  ( -1.000000000000000000, 0.000000000000000000, 0.000000000000000000 ) ) ;
#8748=VERTEX_POINT ( 'NONE', #18146 ) ;
#8752=CARTESIAN_POINT ( 'NONE',  ( 4.999999999999999112, 0.000000000000000000, 0.000000000000000000 ) ) ;
#8765=EDGE_LOOP ( 'NONE', ( #9972, #2864, #250, #5350 ) ) ;
#8771=EDGE_CURVE ( 'NONE', #19381, #9225, #12787, .T. ) ;
#8779=DIRECTION ( 'NONE',  ( -1.000000000000000000, 0.000000000000000000, -0.000000000000000000 ) ) ;
#8782=CARTESIAN_POINT ( 'NONE',  ( 0.000000000000000000, 5.538577986808997267, -6.772677083992326708 ) ) ;
#8788=AXIS2_PLACEMENT_3D ( 'NONE', #3809, #18529, #5731 ) ;
#8796=AXIS2_PLACEMENT_3D ( 'NONE', #8007, #2238, #4041 ) ;
#8813=DIRECTION ( 'NONE',  ( -1.000000000000000000, 0.000000000000000000, 0.000000000000000000 ) ) ;
#8814=CIRCLE ( 'NONE', #2664, 8.749000000000004107 ) ;
#8819=CIRCLE ( 'NONE', #11887, 4.000000000000000000 ) ;
#8820=ORIENTED_EDGE ( 'NONE', *, *, #12356, .T. ) ;
#8830=ORIENTED_EDGE ( 'NONE', *, *, #2346, .F. ) ;
#8833=ADVANCED_FACE ( 'NONE', ( #9417 ), #16707, .T. ) ;
#8853=LINE ( 'NONE', #16264, #23550 ) ;
#8855=CIRCLE ( 'NONE', #22197, 4.000000000000000888 ) ;
#8867=LINE ( 'NONE', #8736, #10652 ) ;
#8874=FACE_OUTER_BOUND ( 'NONE', #6689, .T. ) ;
#8878=DIRECTION ( 'NONE',  ( 0.000000000000000000, -0.5877852522924801315, 0.8090169943749423442 ) ) ;
#8879=EDGE_LOOP ( 'NONE', ( #2842, #8506, #2571, #8718 ) ) ;
#8888=CARTESIAN_POINT ( 'NONE',  ( 4.999999999999999112, 9.314797388894909602, -1.239665997526783858 ) ) ;
#8900=ADVANCED_FACE ( 'NONE', ( #4577 ), #10350, .T. ) ;
#8907=EDGE_LOOP ( 'NONE', ( #16172, #10476, #6687, #20725 ) ) ;
#8917=ORIENTED_EDGE ( 'NONE', *, *, #4528, .F. ) ;
#8929=CYLINDRICAL_SURFACE ( 'NONE', #16739, 8.749000000000002331 ) ;
#8932=EDGE_CURVE ( 'NONE', #22668, #22906, #11787, .T. ) ;
#8935=AXIS2_PLACEMENT_3D ( 'NONE', #14891, #12973, #13207 ) ;
#8936=CARTESIAN_POINT ( 'NONE',  ( 4.999999999999999112, 3.174628368996190719, -8.152713396088728359 ) ) ;
#8937=VERTEX_POINT ( 'NONE', #13821 ) ;
#8939=CARTESIAN_POINT ( 'NONE',  ( 0.000000000000000000, -8.264486777890139635, 4.472189673936757259 ) ) ;
#8940=ORIENTED_EDGE ( 'NONE', *, *, #14340, .F. ) ;
#8944=VECTOR ( 'NONE', #22993, 1000.000000000000000 ) ;
#8948=EDGE_CURVE ( 'NONE', #3346, #2006, #10245, .T. ) ;
#8951=CARTESIAN_POINT ( 'NONE',  ( 4.999999999999999112, 6.478011392632890164, 6.807171995660607600 ) ) ;
#8957=DIRECTION ( 'NONE',  ( -1.000000000000000000, 0.000000000000000000, 0.000000000000000000 ) ) ;
#8959=AXIS2_PLACEMENT_3D ( 'NONE', #12829, #5497, #3816 ) ;
#8971=ORIENTED_EDGE ( 'NONE', *, *, #7093, .T. ) ;
#8984=DIRECTION ( 'NONE',  ( 0.000000000000000000, -1.000000000000000000, 0.000000000000000000 ) ) ;
#8985=ORIENTED_EDGE ( 'NONE', *, *, #10726, .T. ) ;
#8990=DIRECTION ( 'NONE',  ( 1.000000000000000000, -0.000000000000000000, -0.000000000000000000 ) ) ;
#8993=DIRECTION ( 'NONE',  ( 0.000000000000000000, -0.3090169943749347947, -0.9510565162951576390 ) ) ;
#9004=EDGE_CURVE ( 'NONE', #2984, #10612, #23300, .T. ) ;
#9009=ORIENTED_EDGE ( 'NONE', *, *, #6933, .F. ) ;
#9013=LINE ( 'NONE', #3700, #5756 ) ;
#9018=VECTOR ( 'NONE', #571, 1000.000000000000000 ) ;
#9031=EDGE_LOOP ( 'NONE', ( #73, #10521, #6366, #7957 ) ) ;
#9046=DIRECTION ( 'NONE',  ( -1.000000000000000000, -0.000000000000000000, 0.000000000000000000 ) ) ;
#9048=FACE_OUTER_BOUND ( 'NONE', #23166, .T. ) ;
#9052=ORIENTED_EDGE ( 'NONE', *, *, #4155, .T. ) ;
#9057=( LENGTH_UNIT ( ) NAMED_UNIT ( * ) SI_UNIT ( .MILLI., .METRE. ) );
#9060=ORIENTED_EDGE ( 'NONE', *, *, #3938, .T. ) ;
#9062=ORIENTED_EDGE ( 'NONE', *, *, #23074, .T. ) ;
#9068=FACE_OUTER_BOUND ( 'NONE', #18346, .T. ) ;
#9081=CARTESIAN_POINT ( 'NONE',  ( -10.00000000000000000, 0.000000000000000000, 0.000000000000000000 ) ) ;
#9082=ORIENTED_EDGE ( 'NONE', *, *, #15696, .F. ) ;
#9088=DIRECTION ( 'NONE',  ( -1.000000000000000000, 0.000000000000000000, 0.000000000000000000 ) ) ;
#9092=ORIENTED_EDGE ( 'NONE', *, *, #6897, .T. ) ;
#9098=DIRECTION ( 'NONE',  ( -1.000000000000000000, -0.000000000000000000, 0.000000000000000000 ) ) ;
#9125=DIRECTION ( 'NONE',  ( -1.000000000000000000, 0.000000000000000000, 0.000000000000000000 ) ) ;
#9127=CIRCLE ( 'NONE', #1437, 11.00000000000000000 ) ;
#9130=LINE ( 'NONE', #5395, #22593 ) ;
#9131=AXIS2_PLACEMENT_3D ( 'NONE', #7267, #16356, #3755 ) ;
#9133=CARTESIAN_POINT ( 'NONE',  ( 4.999999999999999112, 0.000000000000000000, 0.000000000000000000 ) ) ;
#9137=DIRECTION ( 'NONE',  ( 0.000000000000000000, 0.000000000000000000, -1.000000000000000000 ) ) ;
#9144=AXIS2_PLACEMENT_3D ( 'NONE', #3124, #15619, #10588 ) ;
#9146=DIRECTION ( 'NONE',  ( 0.000000000000000000, 0.000000000000000000, 1.000000000000000000 ) ) ;
#9159=EDGE_LOOP ( 'NONE', ( #7649, #23592, #5829, #8177 ) ) ;
#9172=AXIS2_PLACEMENT_3D ( 'NONE', #18072, #21276, #1180 ) ;
#9175=VECTOR ( 'NONE', #20104, 1000.000000000000000 ) ;
#9178=ORIENTED_EDGE ( 'NONE', *, *, #12356, .F. ) ;
#9181=ORIENTED_EDGE ( 'NONE', *, *, #5865, .T. ) ;
#9185=ORIENTED_EDGE ( 'NONE', *, *, #1837, .F. ) ;
#9190=DIRECTION ( 'NONE',  ( -1.000000000000000000, -0.000000000000000000, -0.000000000000000000 ) ) ;
#9191=ORIENTED_EDGE ( 'NONE', *, *, #18062, .F. ) ;
#9195=CIRCLE ( 'NONE', #17595, 4.000000000000001776 ) ;
#9197=DIRECTION ( 'NONE',  ( -1.000000000000000000, 0.000000000000000000, -0.000000000000000000 ) ) ;
#9198=DIRECTION ( 'NONE',  ( 1.000000000000000000, -0.000000000000000000, -0.000000000000000000 ) ) ;
#9204=ADVANCED_FACE ( 'NONE', ( #11169, #9359 ), #14284, .F. ) ;
#9209=LINE ( 'NONE', #21742, #18918 ) ;
#9212=VERTEX_POINT ( 'NONE', #2138 ) ;
#9221=AXIS2_PLACEMENT_3D ( 'NONE', #154, #16574, #9401 ) ;
#9225=VERTEX_POINT ( 'NONE', #22255 ) ;
#9238=CYLINDRICAL_SURFACE ( 'NONE', #17358, 4.000000000000001776 ) ;
#9248=CARTESIAN_POINT ( 'NONE',  ( -20.00005079999999680, 0.000000000000000000, 4.000000000000000000 ) ) ;
#9255=ORIENTED_EDGE ( 'NONE', *, *, #17706, .F. ) ;
#9265=CARTESIAN_POINT ( 'NONE',  ( 4.999999999999999112, 9.241976615262133876, 1.699438267350532827 ) ) ;
#9275=ORIENTED_EDGE ( 'NONE', *, *, #5455, .T. ) ;
#9292=( LENGTH_UNIT ( ) NAMED_UNIT ( * ) SI_UNIT ( .MILLI., .METRE. ) );
#9294=AXIS2_PLACEMENT_3D ( 'NONE', #8721, #17932, #21145 ) ;
#9303=DIRECTION ( 'NONE',  ( 0.000000000000000000, 0.000000000000000000, -1.000000000000000000 ) ) ;
#9305=DIRECTION ( 'NONE',  ( -1.000000000000000000, -0.000000000000000000, -0.000000000000000000 ) ) ;
#9306=CYLINDRICAL_SURFACE ( 'NONE', #18722, 8.749000000000002331 ) ;
#9319=DIRECTION ( 'NONE',  ( 0.000000000000000000, 0.000000000000000000, -1.000000000000000000 ) ) ;
#9326=CIRCLE ( 'NONE', #10486, 4.000000000000001776 ) ;
#9352=ORIENTED_EDGE ( 'NONE', *, *, #22256, .T. ) ;
#9354=VERTEX_POINT ( 'NONE', #2614 ) ;
#9359=FACE_BOUND ( 'NONE', #17332, .T. ) ;
#9363=VERTEX_POINT ( 'NONE', #9833 ) ;
#9369=FACE_OUTER_BOUND ( 'NONE', #9159, .T. ) ;
#9376=ORIENTED_EDGE ( 'NONE', *, *, #13631, .T. ) ;
#9393=DIRECTION ( 'NONE',  ( 0.000000000000000000, 0.000000000000000000, 1.000000000000000000 ) ) ;
#9401=DIRECTION ( 'NONE',  ( 0.000000000000000000, 0.000000000000000000, -1.000000000000000000 ) ) ;
#9404=CARTESIAN_POINT ( 'NONE',  ( 0.000000000000000000, -8.264486777890077462, -4.472189673936873611 ) ) ;
#9405=VERTEX_POINT ( 'NONE', #17485 ) ;
#9411=ORIENTED_EDGE ( 'NONE', *, *, #10808, .T. ) ;
#9417=FACE_OUTER_BOUND ( 'NONE', #1011, .T. ) ;
#9432=CYLINDRICAL_SURFACE ( 'NONE', #2553, 8.749000000000002331 ) ;
#9452=DIRECTION ( 'NONE',  ( 0.000000000000000000, 0.000000000000000000, 1.000000000000000000 ) ) ;
#9455=VERTEX_POINT ( 'NONE', #2847 ) ;
#9462=FACE_OUTER_BOUND ( 'NONE', #8227, .T. ) ;
#9470=VECTOR ( 'NONE', #6659, 1000.000000000000000 ) ;
#9472=DIRECTION ( 'NONE',  ( -1.000000000000000000, -0.000000000000000000, -0.000000000000000000 ) ) ;
#9477=AXIS2_PLACEMENT_3D ( 'NONE', #22589, #6192, #11961 ) ;
#9479=CARTESIAN_POINT ( 'NONE',  ( 4.999999999999999112, 0.000000000000000000, 0.000000000000000000 ) ) ;
#9499=ORIENTED_EDGE ( 'NONE', *, *, #4531, .F. ) ;
#9500=CIRCLE ( 'NONE', #13705, 11.00000000000000000 ) ;
#9502=ORIENTED_EDGE ( 'NONE', *, *, #20277, .F. ) ;
#9509=MECHANICAL_DESIGN_GEOMETRIC_PRESENTATION_REPRESENTATION('',(#696),#9909);
#9523=CARTESIAN_POINT ( 'NONE',  ( 4.999999999999999112, 8.734705317681626724, 0.4999240074894746311 ) ) ;
#9556=AXIS2_PLACEMENT_3D ( 'NONE', #21855, #65, #14709 ) ;
#9568=ORIENTED_EDGE ( 'NONE', *, *, #13309, .T. ) ;
#9569=ADVANCED_FACE ( 'NONE', ( #5367 ), #19846, .T. ) ;
#9571=UNCERTAINTY_MEASURE_WITH_UNIT (LENGTH_MEASURE( 1.000000000000000082E-05 ), #5510, 'distance_accuracy_value', 'NONE');
#9575=VECTOR ( 'NONE', #16717, 1000.000000000000000 ) ;
#9577=VERTEX_POINT ( 'NONE', #21514 ) ;
#9592=ORIENTED_EDGE ( 'NONE', *, *, #14943, .F. ) ;
#9593=CARTESIAN_POINT ( 'NONE',  ( 0.000000000000000000, -9.680994141368733708, -5.222868219166961978 ) ) ;
#9596=AXIS2_PLACEMENT_3D ( 'NONE', #10116, #6269, #11800 ) ;
#9599=EDGE_LOOP ( 'NONE', ( #9181, #21903, #12446, #17382 ) ) ;
#9610=VECTOR ( 'NONE', #17512, 1000.000000000000000 ) ;
#9616=DIRECTION ( 'NONE',  ( 0.000000000000000000, 0.000000000000000000, 1.000000000000000000 ) ) ;
#9631=AXIS2_PLACEMENT_3D ( 'NONE', #11768, #22865, #15477 ) ;
#9660=DIRECTION ( 'NONE',  ( 0.000000000000000000, 0.000000000000000000, 1.000000000000000000 ) ) ;
#9673=ORIENTED_EDGE ( 'NONE', *, *, #5551, .F. ) ;
#9677=EDGE_LOOP ( 'NONE', ( #9191, #1772, #4978, #8620 ) ) ;
#9678=ORIENTED_EDGE ( 'NONE', *, *, #20160, .T. ) ;
#9687=EDGE_CURVE ( 'NONE', #2340, #22874, #5729, .T. ) ;
#9695=FACE_OUTER_BOUND ( 'NONE', #10043, .T. ) ;
#9696=EDGE_CURVE ( 'NONE', #22762, #9455, #9961, .T. ) ;
#9709=CARTESIAN_POINT ( 'NONE',  ( 4.999999999999999112, 10.82112760146736363, 1.975651141462276161 ) ) ;
#9721=EDGE_CURVE ( 'NONE', #1063, #6899, #7660, .T. ) ;
#9725=EDGE_CURVE ( 'NONE', #14838, #2957, #20262, .T. ) ;
#9729=CARTESIAN_POINT ( 'NONE',  ( 4.999999999999999112, -8.461683424509297780, -2.223716399045659653 ) ) ;
#9742=EDGE_LOOP ( 'NONE', ( #100, #9062, #2641, #131 ) ) ;
#9757=ORIENTED_EDGE ( 'NONE', *, *, #22047, .F. ) ;
#9773=CARTESIAN_POINT ( 'NONE',  ( 4.999999999999999112, 1.239665997526886665, 9.314797388894895391 ) ) ;
#9780=AXIS2_PLACEMENT_3D ( 'NONE', #20794, #2243, #9935 ) ;
#9786=ORIENTED_EDGE ( 'NONE', *, *, #23599, .F. ) ;
#9792=EDGE_CURVE ( 'NONE', #14716, #5267, #17609, .T. ) ;
#9797=CARTESIAN_POINT ( 'NONE',  ( -10.00000000000000000, 0.000000000000000000, 0.000000000000000000 ) ) ;
#9801=EDGE_CURVE ( 'NONE', #2890, #2006, #10360, .T. ) ;
#9808=DIRECTION ( 'NONE',  ( -1.000000000000000000, 0.000000000000000000, 0.000000000000000000 ) ) ;
#9825=EDGE_LOOP ( 'NONE', ( #9502, #7998, #2097, #23401 ) ) ;
#9833=CARTESIAN_POINT ( 'NONE',  ( -20.00005079999999680, 4.898587196589412829E-16, -4.000000000000000000 ) ) ;
#9836=ORIENTED_EDGE ( 'NONE', *, *, #2170, .T. ) ;
#9837=DIRECTION ( 'NONE',  ( 0.000000000000000000, 0.9510565162951521989, 0.3090169943749515591 ) ) ;
#9842=CARTESIAN_POINT ( 'NONE',  ( 4.999999999999999112, -4.472189673936844301, 8.264486777890091673 ) ) ;
#9846=DIRECTION ( 'NONE',  ( 1.000000000000000000, 0.000000000000000000, 0.000000000000000000 ) ) ;
#9847=DIRECTION ( 'NONE',  ( 0.000000000000000000, 0.000000000000000000, 1.000000000000000000 ) ) ;
#9848=ORIENTED_EDGE ( 'NONE', *, *, #18165, .T. ) ;
#9850=ORIENTED_EDGE ( 'NONE', *, *, #1837, .T. ) ;
#9857=ORIENTED_EDGE ( 'NONE', *, *, #14069, .F. ) ;
#9864=CIRCLE ( 'NONE', #267, 4.000000000000001776 ) ;
#9865=EDGE_CURVE ( 'NONE', #12130, #16102, #17890, .T. ) ;
#9871=DIRECTION ( 'NONE',  ( 0.000000000000000000, 0.9510565162951544194, -0.3090169943749447312 ) ) ;
#9879=CIRCLE ( 'NONE', #14461, 8.749000000000002331 ) ;
#9897=CIRCLE ( 'NONE', #11429, 4.000000000000002665 ) ;
#9909=( GEOMETRIC_REPRESENTATION_CONTEXT ( 3 ) GLOBAL_UNCERTAINTY_ASSIGNED_CONTEXT ( ( #9571 ) ) GLOBAL_UNIT_ASSIGNED_CONTEXT ( ( #5510, #114, #21793 ) ) REPRESENTATION_CONTEXT ( 'NONE', 'WORKASPACE' ) );
#9912=VERTEX_POINT ( 'NONE', #5189 ) ;
#9916=EDGE_LOOP ( 'NONE', ( #8820, #12731, #827, #16414, #14958, #22208 ) ) ;
#9923=DIRECTION ( 'NONE',  ( -1.000000000000000000, -0.000000000000000000, 0.000000000000000000 ) ) ;
#9926=AXIS2_PLACEMENT_3D ( 'NONE', #6113, #591, #9837 ) ;
#9929=EDGE_CURVE ( 'NONE', #9912, #22668, #21789, .T. ) ;
#9935=DIRECTION ( 'NONE',  ( 0.000000000000000000, 0.5877852522924684742, 0.8090169943749507819 ) ) ;
#9937=ORIENTED_EDGE ( 'NONE', *, *, #15476, .T. ) ;
#9944=ORIENTED_EDGE ( 'NONE', *, *, #21343, .F. ) ;
#9947=CARTESIAN_POINT ( 'NONE',  ( 2.499999999999999556, -7.593217523260641144, 7.958834565716742304 ) ) ;
#9948=DIRECTION ( 'NONE',  ( -1.000000000000000000, 0.000000000000000000, -0.000000000000000000 ) ) ;
#9961=CIRCLE ( 'NONE', #16071, 11.00000000000000000 ) ;
#9964=CARTESIAN_POINT ( 'NONE',  ( 0.000000000000000000, 0.000000000000000000, 0.000000000000000000 ) ) ;
#9972=ORIENTED_EDGE ( 'NONE', *, *, #12351, .T. ) ;
#9975=DIRECTION ( 'NONE',  ( 0.000000000000000000, 0.000000000000000000, 1.000000000000000000 ) ) ;
#9978=ADVANCED_FACE ( 'NONE', ( #11318 ), #11075, .T. ) ;
#9984=VERTEX_POINT ( 'NONE', #6021 ) ;
#9997=EDGE_CURVE ( 'NONE', #12317, #15248, #4214, .T. ) ;
#10000=FACE_OUTER_BOUND ( 'NONE', #1174, .T. ) ;
#10006=CIRCLE ( 'NONE', #4631, 4.000000000000001776 ) ;
#10015=ORIENTED_EDGE ( 'NONE', *, *, #6402, .T. ) ;
#10024=AXIS2_PLACEMENT_3D ( 'NONE', #15098, #18532, #3574 ) ;
#10033=DIRECTION ( 'NONE',  ( -1.000000000000000000, -0.000000000000000000, -0.000000000000000000 ) ) ;
#10043=EDGE_LOOP ( 'NONE', ( #11752, #16765, #4191, #1135 ) ) ;
#10061=CARTESIAN_POINT ( 'NONE',  ( 0.000000000000000000, 10.82112760146739383, -1.975651141462125171 ) ) ;
#10063=ORIENTED_EDGE ( 'NONE', *, *, #12379, .T. ) ;
#10069=CARTESIAN_POINT ( 'NONE',  ( 4.999999999999999112, 4.472189673936787457, 8.264486777890123648 ) ) ;
#10072=AXIS2_PLACEMENT_3D ( 'NONE', #1091, #6622, #21198 ) ;
#10076=DIRECTION ( 'NONE',  ( 0.000000000000000000, -6.938893903907226800E-15, 1.000000000000000000 ) ) ;
#10080=ORIENTED_EDGE ( 'NONE', *, *, #5101, .F. ) ;
#10086=CARTESIAN_POINT ( 'NONE',  ( 4.999999999999999112, 4.729683950898872169, 7.360373001730934561 ) ) ;
#10102=ORIENTED_EDGE ( 'NONE', *, *, #19023, .F. ) ;
#10116=CARTESIAN_POINT ( 'NONE',  ( 4.999999999999999112, 9.314797388894893615, 1.239665997526919083 ) ) ;
#10117=ORIENTED_EDGE ( 'NONE', *, *, #1504, .F. ) ;
#10119=ORIENTED_EDGE ( 'NONE', *, *, #1015, .F. ) ;
#10147=CARTESIAN_POINT ( 'NONE',  ( -10.00000000000000000, 0.000000000000000000, 0.000000000000000000 ) ) ;
#10151=CARTESIAN_POINT ( 'NONE',  ( 0.000000000000000000, -8.152713396088739017, -3.174628368996162298 ) ) ;
#10152=EDGE_LOOP ( 'NONE', ( #10864, #10833, #5291, #8178 ) ) ;
#10171=AXIS2_PLACEMENT_3D ( 'NONE', #10990, #3545, #10881 ) ;
#10178=DIRECTION ( 'NONE',  ( -1.000000000000000000, -0.000000000000000000, -0.000000000000000000 ) ) ;
#10182=LINE ( 'NONE', #23436, #3908 ) ;
#10184=DIRECTION ( 'NONE',  ( 1.000000000000000000, -0.000000000000000000, -0.000000000000000000 ) ) ;
#10206=EDGE_CURVE ( 'NONE', #10458, #12128, #22946, .T. ) ;
#10207=DIRECTION ( 'NONE',  ( 0.000000000000000000, 0.000000000000000000, 1.000000000000000000 ) ) ;
#10211=CARTESIAN_POINT ( 'NONE',  ( -10.00000000000000000, 0.000000000000000000, 0.000000000000000000 ) ) ;
#10215=ORIENTED_EDGE ( 'NONE', *, *, #22325, .F. ) ;
#10230=ADVANCED_FACE ( 'NONE', ( #22538 ), #19064, .T. ) ;
#10240=ORIENTED_EDGE ( 'NONE', *, *, #15677, .T. ) ;
#10244=VERTEX_POINT ( 'NONE', #2530 ) ;
#10245=CIRCLE ( 'NONE', #23601, 11.00000000000000000 ) ;
#10247=ORIENTED_EDGE ( 'NONE', *, *, #15382, .T. ) ;
#10257=CARTESIAN_POINT ( 'NONE',  ( 4.999999999999999112, 0.000000000000000000, 0.000000000000000000 ) ) ;
#10266=DIRECTION ( 'NONE',  ( -1.000000000000000000, 0.000000000000000000, -0.000000000000000000 ) ) ;
#10281=CARTESIAN_POINT ( 'NONE',  ( 0.000000000000000000, 1.699438267350500409, -9.241976615262139205 ) ) ;
#10290=DIRECTION ( 'NONE',  ( -1.000000000000000000, 0.000000000000000000, 0.000000000000000000 ) ) ;
#10301=FACE_OUTER_BOUND ( 'NONE', #5581, .T. ) ;
#10303=DIRECTION ( 'NONE',  ( 0.000000000000000000, 0.000000000000000000, -1.000000000000000000 ) ) ;
#10311=CARTESIAN_POINT ( 'NONE',  ( 4.999999999999999112, 4.729683950898872169, 7.360373001730934561 ) ) ;
#10327=VECTOR ( 'NONE', #17097, 1000.000000000000000 ) ;
#10329=ORIENTED_EDGE ( 'NONE', *, *, #22325, .T. ) ;
#10330=FACE_OUTER_BOUND ( 'NONE', #20604, .T. ) ;
#10341=AXIS2_PLACEMENT_3D ( 'NONE', #14175, #8779, #13829 ) ;
#10342=VERTEX_POINT ( 'NONE', #12378 ) ;
#10343=FACE_OUTER_BOUND ( 'NONE', #22430, .T. ) ;
#10349=CIRCLE ( 'NONE', #21386, 8.749000000000002331 ) ;
#10350=CYLINDRICAL_SURFACE ( 'NONE', #8313, 4.000000000000001776 ) ;
#10360=CIRCLE ( 'NONE', #3830, 4.000000000000001776 ) ;
#10364=ORIENTED_EDGE ( 'NONE', *, *, #6331, .F. ) ;
#10385=AXIS2_PLACEMENT_3D ( 'NONE', #13436, #9472, #4305 ) ;
#10397=ORIENTED_EDGE ( 'NONE', *, *, #252, .T. ) ;
#10403=DIRECTION ( 'NONE',  ( -1.000000000000000000, 0.000000000000000000, -0.000000000000000000 ) ) ;
#10406=AXIS2_PLACEMENT_3D ( 'NONE', #9842, #19380, #22989 ) ;
#10415=DIRECTION ( 'NONE',  ( 0.000000000000000000, -0.8090169943749403458, -0.5877852522924831291 ) ) ;
#10421=ORIENTED_EDGE ( 'NONE', *, *, #6933, .T. ) ;
#10426=DIRECTION ( 'NONE',  ( -1.000000000000000000, 0.000000000000000000, 0.000000000000000000 ) ) ;
#10427=DIRECTION ( 'NONE',  ( 0.000000000000000000, 0.000000000000000000, 1.000000000000000000 ) ) ;
#10430=ORIENTED_EDGE ( 'NONE', *, *, #4646, .F. ) ;
#10440=ORIENTED_EDGE ( 'NONE', *, *, #20798, .F. ) ;
#10446=CARTESIAN_POINT ( 'NONE',  ( 4.999999999999999112, -6.772677083992345359, -5.538577986808975062 ) ) ;
#10452=VECTOR ( 'NONE', #569, 1000.000000000000000 ) ;
#10453=EDGE_LOOP ( 'NONE', ( #992, #9857, #22524, #10397 ) ) ;
#10455=CARTESIAN_POINT ( 'NONE',  ( 25.00005080000000035, 5.400000000000000355, 1.000000000000000000 ) ) ;
#10458=VERTEX_POINT ( 'NONE', #15848 ) ;
#10459=DIRECTION ( 'NONE',  ( 0.000000000000000000, 0.000000000000000000, -1.000000000000000000 ) ) ;
#10460=VERTEX_POINT ( 'NONE', #7218 ) ;
#10476=ORIENTED_EDGE ( 'NONE', *, *, #3730, .F. ) ;
#10486=AXIS2_PLACEMENT_3D ( 'NONE', #8081, #17166, #8189 ) ;
#10492=CARTESIAN_POINT ( 'NONE',  ( 2.499999999999999556, -10.82112760146737962, 1.975651141462196225 ) ) ;
#10507=DIRECTION ( 'NONE',  ( 0.000000000000000000, 0.000000000000000000, 1.000000000000000000 ) ) ;
#10517=DIRECTION ( 'NONE',  ( 0.000000000000000000, 0.3090169943749481174, -0.9510565162951533091 ) ) ;
#10518=ORIENTED_EDGE ( 'NONE', *, *, #6931, .T. ) ;
#10521=ORIENTED_EDGE ( 'NONE', *, *, #12913, .T. ) ;
#10526=CARTESIAN_POINT ( 'NONE',  ( 4.999999999999999112, 9.241976615262160522, -1.699438267350405818 ) ) ;
#10532=DIRECTION ( 'NONE',  ( 0.000000000000000000, 0.000000000000000000, 1.000000000000000000 ) ) ;
#10535=ORIENTED_EDGE ( 'NONE', *, *, #12913, .F. ) ;
#10538=DIRECTION ( 'NONE',  ( 1.000000000000000000, 0.000000000000000000, -0.000000000000000000 ) ) ;
#10541=DIRECTION ( 'NONE',  ( -1.000000000000000000, 0.000000000000000000, -0.000000000000000000 ) ) ;
#10553=DIRECTION ( 'NONE',  ( -1.000000000000000000, -0.000000000000000000, -0.000000000000000000 ) ) ;
#10554=CARTESIAN_POINT ( 'NONE',  ( -20.00005080000000035, 0.000000000000000000, 0.000000000000000000 ) ) ;
#10557=CARTESIAN_POINT ( 'NONE',  ( 0.000000000000000000, 0.000000000000000000, 0.000000000000000000 ) ) ;
#10559=DIRECTION ( 'NONE',  ( 0.000000000000000000, 0.000000000000000000, 1.000000000000000000 ) ) ;
#10570=AXIS2_PLACEMENT_3D ( 'NONE', #21140, #8599, #10532 ) ;
#10573=ORIENTED_EDGE ( 'NONE', *, *, #12757, .T. ) ;
#10577=ADVANCED_FACE ( 'NONE', ( #14885 ), #5760, .T. ) ;
#10588=DIRECTION ( 'NONE',  ( 0.000000000000000000, 0.000000000000000000, -1.000000000000000000 ) ) ;
#10595=EDGE_CURVE ( 'NONE', #16281, #1668, #12619, .T. ) ;
#10612=VERTEX_POINT ( 'NONE', #16427 ) ;
#10620=DIRECTION ( 'NONE',  ( 0.000000000000000000, 1.000000000000000000, 3.491481338843133355E-15 ) ) ;
#10631=EDGE_CURVE ( 'NONE', #22912, #6574, #14647, .T. ) ;
#10637=EDGE_LOOP ( 'NONE', ( #8917, #6607, #4677, #14188, #18038, #1780, #22331, #6111, #6545, #545, #18726, #952, #10535, #9255, #20890, #22456, #18984, #19861, #22982, #22192, #7549, #15855, #1096, #4851, #11526, #9499, #15478, #11307, #15310, #12073, #6937, #2096, #16560, #3855, #9786, #7515, #6865, #15666, #17139, #10102, #6013, #3690, #10364, #22327, #18313, #10117, #13792, #1046, #12420, #6090, #4654, #14712, #5450, #4171, #3097, #18433, #13980, #5912, #20696, #22028, #221, #20839, #8612, #10978, #16498, #9757, #11959, #755, #4496, #23170, #20626, #14474, #10759, #14998, #16026, #22248, #5872, #2316, #10119, #19708, #15074, #21893, #3254, #6229, #19661 ) ) ;
#10638=CIRCLE ( 'NONE', #2944, 8.749000000000002331 ) ;
#10652=VECTOR ( 'NONE', #14613, 1000.000000000000000 ) ;
#10653=CARTESIAN_POINT ( 'NONE',  ( 0.000000000000000000, -1.239665997526951724, 9.314797388894888286 ) ) ;
#10659=ORIENTED_EDGE ( 'NONE', *, *, #16158, .T. ) ;
#10660=DIRECTION ( 'NONE',  ( 0.000000000000000000, 0.3090169943749412895, 0.9510565162951556406 ) ) ;
#10664=DIRECTION ( 'NONE',  ( -1.000000000000000000, 0.000000000000000000, 0.000000000000000000 ) ) ;
#10673=CIRCLE ( 'NONE', #3372, 4.000000000000001776 ) ;
#10680=CYLINDRICAL_SURFACE ( 'NONE', #15887, 4.000000000000001776 ) ;
#10686=DIRECTION ( 'NONE',  ( 0.000000000000000000, 0.000000000000000000, 1.000000000000000000 ) ) ;
#10696=DIRECTION ( 'NONE',  ( -1.000000000000000000, 0.000000000000000000, 0.000000000000000000 ) ) ;
#10726=EDGE_CURVE ( 'NONE', #3902, #17992, #710, .T. ) ;
#10735=CARTESIAN_POINT ( 'NONE',  ( 0.000000000000000000, -9.915734732513184824, -4.762163868918378284 ) ) ;
#10742=EDGE_CURVE ( 'NONE', #10755, #19924, #13444, .T. ) ;
#10755=VERTEX_POINT ( 'NONE', #2504 ) ;
#10759=ORIENTED_EDGE ( 'NONE', *, *, #23074, .F. ) ;
#10764=CIRCLE ( 'NONE', #398, 4.000000000000000888 ) ;
#10766=ADVANCED_FACE ( 'NONE', ( #21052 ), #18914, .T. ) ;
#10780=EDGE_LOOP ( 'NONE', ( #135, #9673, #1048, #5256 ) ) ;
#10782=CARTESIAN_POINT ( 'NONE',  ( 4.999999999999999112, 0.000000000000000000, 0.000000000000000000 ) ) ;
#10783=CARTESIAN_POINT ( 'NONE',  ( 4.999999999999999112, 8.264486777890107660, -4.472189673936815879 ) ) ;
#10784=ORIENTED_EDGE ( 'NONE', *, *, #2370, .T. ) ;
#10794=DIRECTION ( 'NONE',  ( -1.000000000000000000, -0.000000000000000000, 0.000000000000000000 ) ) ;
#10798=DIRECTION ( 'NONE',  ( -1.000000000000000000, 0.000000000000000000, 0.000000000000000000 ) ) ;
#10800=CARTESIAN_POINT ( 'NONE',  ( 0.000000000000000000, 0.000000000000000000, 0.000000000000000000 ) ) ;
#10808=EDGE_CURVE ( 'NONE', #3506, #17633, #23338, .T. ) ;
#10814=ORIENTED_EDGE ( 'NONE', *, *, #9997, .F. ) ;
#10827=LINE ( 'NONE', #14415, #4613 ) ;
#10833=ORIENTED_EDGE ( 'NONE', *, *, #8370, .F. ) ;
#10852=CARTESIAN_POINT ( 'NONE',  ( 2.499999999999999556, 1.975651141462390514, -10.82112760146734232 ) ) ;
#10853=CIRCLE ( 'NONE', #20381, 8.749000000000002331 ) ;
#10864=ORIENTED_EDGE ( 'NONE', *, *, #2370, .F. ) ;
#10869=DIRECTION ( 'NONE',  ( 1.000000000000000000, -0.000000000000000000, 0.000000000000000000 ) ) ;
#10870=ADVANCED_FACE ( 'NONE', ( #17612 ), #5132, .T. ) ;
#10881=DIRECTION ( 'NONE',  ( 0.000000000000000000, 0.000000000000000000, -1.000000000000000000 ) ) ;
#10885=DIRECTION ( 'NONE',  ( 0.000000000000000000, 0.000000000000000000, 1.000000000000000000 ) ) ;
#10886=ORIENTED_EDGE ( 'NONE', *, *, #1042, .F. ) ;
#10895=ADVANCED_FACE ( 'NONE', ( #8874 ), #5022, .T. ) ;
#10910=EDGE_LOOP ( 'NONE', ( #23640, #6749, #13953, #11451 ) ) ;
#10921=CIRCLE ( 'NONE', #18926, 4.000000000000001776 ) ;
#10932=DIRECTION ( 'NONE',  ( -1.000000000000000000, 0.000000000000000000, 0.000000000000000000 ) ) ;
#10933=AXIS2_PLACEMENT_3D ( 'NONE', #23312, #15569, #23182 ) ;
#10948=ORIENTED_EDGE ( 'NONE', *, *, #10742, .T. ) ;
#10955=VECTOR ( 'NONE', #8167, 1000.000000000000000 ) ;
#10966=ORIENTED_EDGE ( 'NONE', *, *, #19023, .T. ) ;
#10978=ORIENTED_EDGE ( 'NONE', *, *, #7740, .F. ) ;
#10990=CARTESIAN_POINT ( 'NONE',  ( 0.000000000000000000, 8.475820894093034852, -4.057423117305300586 ) ) ;
#11001=ORIENTED_EDGE ( 'NONE', *, *, #2319, .T. ) ;
#11028=DIRECTION ( 'NONE',  ( -1.000000000000000000, 0.000000000000000000, 0.000000000000000000 ) ) ;
#11036=ORIENTED_EDGE ( 'NONE', *, *, #19908, .T. ) ;
#11051=DIRECTION ( 'NONE',  ( -1.000000000000000000, -0.000000000000000000, 0.000000000000000000 ) ) ;
#11065=CARTESIAN_POINT ( 'NONE',  ( 0.000000000000000000, -9.314797388894900720, 5.239665997526855357 ) ) ;
#11075=CYLINDRICAL_SURFACE ( 'NONE', #18312, 4.000000000000001776 ) ;
#11083=VECTOR ( 'NONE', #13410, 1000.000000000000000 ) ;
#11087=ORIENTED_EDGE ( 'NONE', *, *, #17900, .T. ) ;
#11092=CARTESIAN_POINT ( 'NONE',  ( -20.00005079999999680, 5.400000000000000355, -1.000000000000000000 ) ) ;
#11099=EDGE_LOOP ( 'NONE', ( #5370, #20053, #3201, #167 ) ) ;
#11106=CARTESIAN_POINT ( 'NONE',  ( 0.000000000000000000, 8.461683424509345741, -2.223716399045483350 ) ) ;
#11107=AXIS2_PLACEMENT_3D ( 'NONE', #1513, #4875, #16263 ) ;
#11109=CIRCLE ( 'NONE', #12264, 8.749000000000000554 ) ;
#11156=CARTESIAN_POINT ( 'NONE',  ( 4.999999999999999112, -9.314797388894900720, 5.239665997526855357 ) ) ;
#11158=EDGE_CURVE ( 'NONE', #3223, #5947, #15446, .T. ) ;
#11162=ORIENTED_EDGE ( 'NONE', *, *, #14055, .F. ) ;
#11169=FACE_OUTER_BOUND ( 'NONE', #10637, .T. ) ;
#11178=LINE ( 'NONE', #7697, #15380 ) ;
#11185=ORIENTED_EDGE ( 'NONE', *, *, #1665, .F. ) ;
#11188=SHAPE_DEFINITION_REPRESENTATION ( #20982, #16640 ) ;
#11201=DIRECTION ( 'NONE',  ( 0.000000000000000000, 0.000000000000000000, -1.000000000000000000 ) ) ;
#11205=VERTEX_POINT ( 'NONE', #16874 ) ;
#11212=DIRECTION ( 'NONE',  ( -1.000000000000000000, -0.000000000000000000, 0.000000000000000000 ) ) ;
#11215=CYLINDRICAL_SURFACE ( 'NONE', #23636, 4.000000000000001776 ) ;
#11221=AXIS2_PLACEMENT_3D ( 'NONE', #20351, #2396, #11292 ) ;
#11233=FACE_OUTER_BOUND ( 'NONE', #5652, .T. ) ;
#11236=VERTEX_POINT ( 'NONE', #22601 ) ;
#11248=PRODUCT ( 'spur gear_iso_ISO - Spur gear 1M 20T 20PA 5FW ---S20B12H25L8.0S1', 'spur gear_iso_ISO - Spur gear 1M 20T 20PA 5FW ---S20B12H25L8.0S1', '', ( #17032 ) ) ;
#11262=CARTESIAN_POINT ( 'NONE',  ( 4.999999999999999112, -4.057423117305329896, -8.475820894093020641 ) ) ;
#11272=ORIENTED_EDGE ( 'NONE', *, *, #14062, .T. ) ;
#11281=ORIENTED_EDGE ( 'NONE', *, *, #15949, .F. ) ;
#11283=CYLINDRICAL_SURFACE ( 'NONE', #4153, 11.00000000000000000 ) ;
#11292=DIRECTION ( 'NONE',  ( 0.000000000000000000, 0.000000000000000000, 1.000000000000000000 ) ) ;
#11293=CIRCLE ( 'NONE', #15128, 11.00000000000000000 ) ;
#11307=ORIENTED_EDGE ( 'NONE', *, *, #10206, .F. ) ;
#11310=CIRCLE ( 'NONE', #14368, 8.749000000000002331 ) ;
#11318=FACE_OUTER_BOUND ( 'NONE', #19619, .T. ) ;
#11327=EDGE_CURVE ( 'NONE', #15248, #5525, #11178, .T. ) ;
#11333=AXIS2_PLACEMENT_3D ( 'NONE', #17034, #1076, #13568 ) ;
#11353=DIRECTION ( 'NONE',  ( 0.000000000000000000, 0.000000000000000000, -1.000000000000000000 ) ) ;
#11356=CARTESIAN_POINT ( 'NONE',  ( 2.499999999999999556, 9.915734732513218574, 4.762163868918309007 ) ) ;
#11363=ORIENTED_EDGE ( 'NONE', *, *, #19059, .F. ) ;
#11365=VERTEX_POINT ( 'NONE', #18450 ) ;
#11377=CARTESIAN_POINT ( 'NONE',  ( 0.000000000000000000, 0.000000000000000000, 0.000000000000000000 ) ) ;
#11381=CARTESIAN_POINT ( 'NONE',  ( 4.999999999999999112, -10.82112760146737784, 1.975651141462196669 ) ) ;
#11384=VERTEX_POINT ( 'NONE', #18922 ) ;
#11385=CARTESIAN_POINT ( 'NONE',  ( 4.999999999999999112, -8.152713396088739017, -3.174628368996162298 ) ) ;
#11391=ORIENTED_EDGE ( 'NONE', *, *, #1665, .T. ) ;
#11393=ADVANCED_FACE ( 'NONE', ( #20711 ), #15718, .T. ) ;
#11400=DIRECTION ( 'NONE',  ( 1.000000000000000000, -0.000000000000000000, -0.000000000000000000 ) ) ;
#11403=VERTEX_POINT ( 'NONE', #10086 ) ;
#11429=AXIS2_PLACEMENT_3D ( 'NONE', #2930, #10403, #10517 ) ;
#11431=EDGE_CURVE ( 'NONE', #19924, #15228, #13833, .T. ) ;
#11432=ORIENTED_EDGE ( 'NONE', *, *, #22260, .F. ) ;
#11451=ORIENTED_EDGE ( 'NONE', *, *, #21323, .T. ) ;
#11459=DIRECTION ( 'NONE',  ( 0.000000000000000000, 0.000000000000000000, 1.000000000000000000 ) ) ;
#11460=EDGE_CURVE ( 'NONE', #9455, #5926, #21439, .T. ) ;
#11464=AXIS2_PLACEMENT_3D ( 'NONE', #2101, #22095, #18407 ) ;
#11486=VERTEX_POINT ( 'NONE', #19268 ) ;
#11488=DIRECTION ( 'NONE',  ( -1.000000000000000000, 0.000000000000000000, 0.000000000000000000 ) ) ;
#11495=AXIS2_PLACEMENT_3D ( 'NONE', #17694, #10290, #15901 ) ;
#11516=DIRECTION ( 'NONE',  ( 0.000000000000000000, 0.000000000000000000, 1.000000000000000000 ) ) ;
#11519=CARTESIAN_POINT ( 'NONE',  ( 4.999999999999999112, 0.000000000000000000, 0.000000000000000000 ) ) ;
#11526=ORIENTED_EDGE ( 'NONE', *, *, #16449, .F. ) ;
#11529=CARTESIAN_POINT ( 'NONE',  ( 4.999999999999999112, -8.264486777890139635, 4.472189673936757259 ) ) ;
#11533=ORIENTED_EDGE ( 'NONE', *, *, #5457, .T. ) ;
#11535=CARTESIAN_POINT ( 'NONE',  ( 0.000000000000000000, -10.82112760146734765, -1.975651141462352767 ) ) ;
#11544=CARTESIAN_POINT ( 'NONE',  ( -20.00005079999999680, 3.872983346207417021, 1.000000000000000000 ) ) ;
#11564=EDGE_CURVE ( 'NONE', #23470, #17148, #16876, .T. ) ;
#11570=CARTESIAN_POINT ( 'NONE',  ( 4.999999999999999112, -1.975651141462315907, 10.82112760146735475 ) ) ;
#11577=CARTESIAN_POINT ( 'NONE',  ( 25.00005080000000035, 4.898587196589412829E-16, -4.000000000000000000 ) ) ;
#11586=DIRECTION ( 'NONE',  ( 0.000000000000000000, -0.8090169943749402348, -0.5877852522924831291 ) ) ;
#11590=CARTESIAN_POINT ( 'NONE',  ( 4.999999999999999112, 0.000000000000000000, 0.000000000000000000 ) ) ;
#11604=VERTEX_POINT ( 'NONE', #19738 ) ;
#11617=EDGE_CURVE ( 'NONE', #22394, #9212, #10006, .T. ) ;
#11623=FACE_OUTER_BOUND ( 'NONE', #2199, .T. ) ;
#11624=VERTEX_POINT ( 'NONE', #18074 ) ;
#11629=EDGE_CURVE ( 'NONE', #8937, #10755, #8855, .T. ) ;
#11634=AXIS2_PLACEMENT_3D ( 'NONE', #887, #10266, #6655 ) ;
#11644=VERTEX_POINT ( 'NONE', #23095 ) ;
#11658=CARTESIAN_POINT ( 'NONE',  ( 0.000000000000000000, 1.464956435139542323, 10.90201369670499076 ) ) ;
#11659=ADVANCED_FACE ( 'NONE', ( #1654 ), #3216, .T. ) ;
#11669=VERTEX_POINT ( 'NONE', #12241 ) ;
#11674=AXIS2_PLACEMENT_3D ( 'NONE', #2719, #19002, #3078 ) ;
#11692=AXIS2_PLACEMENT_3D ( 'NONE', #17786, #4846, #12305 ) ;
#11694=DIRECTION ( 'NONE',  ( -1.000000000000000000, 0.000000000000000000, -0.000000000000000000 ) ) ;
#11695=ORIENTED_EDGE ( 'NONE', *, *, #2960, .T. ) ;
#11696=EDGE_CURVE ( 'NONE', #17148, #22760, #17838, .T. ) ;
#11701=EDGE_CURVE ( 'NONE', #11669, #21100, #23374, .T. ) ;
#11720=LINE ( 'NONE', #6312, #6029 ) ;
#11726=AXIS2_PLACEMENT_3D ( 'NONE', #19421, #4945, #3017 ) ;
#11734=LINE ( 'NONE', #13167, #11083 ) ;
#11741=DIRECTION ( 'NONE',  ( -1.000000000000000000, 0.000000000000000000, -0.000000000000000000 ) ) ;
#11742=CARTESIAN_POINT ( 'NONE',  ( 0.000000000000000000, 0.000000000000000000, 0.000000000000000000 ) ) ;
#11752=ORIENTED_EDGE ( 'NONE', *, *, #21604, .T. ) ;
#11767=DIRECTION ( 'NONE',  ( 0.000000000000000000, 1.000000000000000000, 3.491481338843133355E-15 ) ) ;
#11768=CARTESIAN_POINT ( 'NONE',  ( -20.00005080000000035, 0.000000000000000000, 0.000000000000000000 ) ) ;
#11772=FACE_OUTER_BOUND ( 'NONE', #10453, .T. ) ;
#11780=DIRECTION ( 'NONE',  ( 0.000000000000000000, 0.000000000000000000, 1.000000000000000000 ) ) ;
#11782=CIRCLE ( 'NONE', #11796, 4.000000000000000888 ) ;
#11783=EDGE_LOOP ( 'NONE', ( #13685, #22598, #681, #9850 ) ) ;
#11787=CIRCLE ( 'NONE', #1024, 8.749000000000002331 ) ;
#11791=EDGE_CURVE ( 'NONE', #5947, #6574, #20296, .T. ) ;
#11796=AXIS2_PLACEMENT_3D ( 'NONE', #21217, #14313, #3029 ) ;
#11800=DIRECTION ( 'NONE',  ( 0.000000000000000000, 0.5877852522924743583, -0.8090169943749467851 ) ) ;
#11801=AXIS2_PLACEMENT_3D ( 'NONE', #18056, #10426, #3442 ) ;
#11811=DIRECTION ( 'NONE',  ( -1.000000000000000000, 0.000000000000000000, 0.000000000000000000 ) ) ;
#11826=FACE_OUTER_BOUND ( 'NONE', #19199, .T. ) ;
#11834=LINE ( 'NONE', #18867, #3066 ) ;
#11838=CYLINDRICAL_SURFACE ( 'NONE', #9477, 4.000000000000001776 ) ;
#11839=VECTOR ( 'NONE', #8984, 1000.000000000000000 ) ;
#11847=VERTEX_POINT ( 'NONE', #5969 ) ;
#11850=VECTOR ( 'NONE', #10869, 1000.000000000000000 ) ;
#11884=DIRECTION ( 'NONE',  ( -1.000000000000000000, -0.000000000000000000, 0.000000000000000000 ) ) ;
#11887=AXIS2_PLACEMENT_3D ( 'NONE', #18630, #2215, #2341 ) ;
#11889=DIRECTION ( 'NONE',  ( 0.000000000000000000, 0.000000000000000000, 1.000000000000000000 ) ) ;
#11904=ORIENTED_EDGE ( 'NONE', *, *, #10742, .F. ) ;
#11935=ADVANCED_FACE ( 'NONE', ( #11623 ), #13646, .T. ) ;
#11946=CYLINDRICAL_SURFACE ( 'NONE', #23076, 8.749000000000002331 ) ;
#11956=CARTESIAN_POINT ( 'NONE',  ( 5.000000000000000000, 5.400000000000000355, 0.000000000000000000 ) ) ;
#11959=ORIENTED_EDGE ( 'NONE', *, *, #5761, .F. ) ;
#11961=DIRECTION ( 'NONE',  ( 0.000000000000000000, 0.000000000000000000, 1.000000000000000000 ) ) ;
#11970=DIRECTION ( 'NONE',  ( -1.000000000000000000, 0.000000000000000000, -0.000000000000000000 ) ) ;
#11978=FACE_OUTER_BOUND ( 'NONE', #20059, .T. ) ;
#11982=CARTESIAN_POINT ( 'NONE',  ( 4.999999999999999112, 8.461683424509345741, -2.223716399045483350 ) ) ;
#12005=CIRCLE ( 'NONE', #504, 4.000000000000001776 ) ;
#12008=DIRECTION ( 'NONE',  ( -1.000000000000000000, -0.000000000000000000, -0.000000000000000000 ) ) ;
#12009=ORIENTED_EDGE ( 'NONE', *, *, #1436, .T. ) ;
#12016=EDGE_LOOP ( 'NONE', ( #17082, #14738, #8985, #499 ) ) ;
#12030=EDGE_CURVE ( 'NONE', #5230, #23216, #8016, .T. ) ;
#12062=FACE_OUTER_BOUND ( 'NONE', #4357, .T. ) ;
#12065=CARTESIAN_POINT ( 'NONE',  ( 0.000000000000000000, 9.241976615262133876, 1.699438267350532827 ) ) ;
#12069=CIRCLE ( 'NONE', #16251, 4.000000000000000888 ) ;
#12072=AXIS2_PLACEMENT_3D ( 'NONE', #22863, #17617, #8280 ) ;
#12073=ORIENTED_EDGE ( 'NONE', *, *, #16217, .F. ) ;
#12081=AXIS2_PLACEMENT_3D ( 'NONE', #13265, #14826, #11353 ) ;
#12085=CARTESIAN_POINT ( 'NONE',  ( 0.000000000000000000, 1.239665997527020558, -9.314797388894877628 ) ) ;
#12095=VERTEX_POINT ( 'NONE', #14241 ) ;
#12097=DIRECTION ( 'NONE',  ( -1.000000000000000000, -0.000000000000000000, -0.000000000000000000 ) ) ;
#12101=VERTEX_POINT ( 'NONE', #13995 ) ;
#12128=VERTEX_POINT ( 'NONE', #5002 ) ;
#12130=VERTEX_POINT ( 'NONE', #19829 ) ;
#12145=DIRECTION ( 'NONE',  ( 0.000000000000000000, 0.3090169943749412895, 0.9510565162951556406 ) ) ;
#12146=EDGE_LOOP ( 'NONE', ( #6834, #16146, #9185, #13860 ) ) ;
#12147=ADVANCED_FACE ( 'NONE', ( #21143 ), #16147, .T. ) ;
#12159=EDGE_CURVE ( 'NONE', #12128, #15377, #1381, .T. ) ;
#12168=CIRCLE ( 'NONE', #19780, 4.000000000000001776 ) ;
#12170=CIRCLE ( 'NONE', #15617, 11.00000000000000000 ) ;
#12171=DIRECTION ( 'NONE',  ( 0.000000000000000000, 0.000000000000000000, 1.000000000000000000 ) ) ;
#12173=ADVANCED_FACE ( 'NONE', ( #10301 ), #7041, .T. ) ;
#12195=AXIS2_PLACEMENT_3D ( 'NONE', #14095, #23415, #4743 ) ;
#12211=COLOUR_RGB ( '', 0.72549020, 0.75294118, 0.79215686) ;
#12216=CARTESIAN_POINT ( 'NONE',  ( 4.999999999999999112, -6.478011392632939014, 6.807171995660559638 ) ) ;
#12220=EDGE_LOOP ( 'NONE', ( #14296, #6284, #5294, #6321 ) ) ;
#12230=CARTESIAN_POINT ( 'NONE',  ( 4.999999999999999112, 0.000000000000000000, 0.000000000000000000 ) ) ;
#12233=APPLICATION_CONTEXT ( 'automotive_design' ) ;
#12234=CARTESIAN_POINT ( 'NONE',  ( 0.000000000000000000, 5.222868219166856285, 9.680994141368792327 ) ) ;
#12241=CARTESIAN_POINT ( 'NONE',  ( 0.000000000000000000, -7.958834565716820464, 7.593217523260554103 ) ) ;
#12243=DIRECTION ( 'NONE',  ( 0.000000000000000000, 0.000000000000000000, 1.000000000000000000 ) ) ;
#12251=CYLINDRICAL_SURFACE ( 'NONE', #4048, 4.000000000000001776 ) ;
#12258=AXIS2_PLACEMENT_3D ( 'NONE', #16956, #291, #6179 ) ;
#12264=AXIS2_PLACEMENT_3D ( 'NONE', #7751, #7631, #5816 ) ;
#12281=VECTOR ( 'NONE', #6187, 1000.000000000000000 ) ;
#12305=DIRECTION ( 'NONE',  ( 0.000000000000000000, -0.9510565162951566398, 0.3090169943749382919 ) ) ;
#12310=CARTESIAN_POINT ( 'NONE',  ( 0.000000000000000000, -9.915734732513254102, 4.762163868918236176 ) ) ;
#12317=VERTEX_POINT ( 'NONE', #21970 ) ;
#12318=DIRECTION ( 'NONE',  ( 0.000000000000000000, -0.9510565162951566398, 0.3090169943749382919 ) ) ;
#12323=DIRECTION ( 'NONE',  ( -1.000000000000000000, -0.000000000000000000, 0.000000000000000000 ) ) ;
#12328=DIRECTION ( 'NONE',  ( 0.000000000000000000, -0.3090169943749349057, -0.9510565162951575280 ) ) ;
#12347=EDGE_CURVE ( 'NONE', #3455, #17148, #5740, .T. ) ;
#12350=CARTESIAN_POINT ( 'NONE',  ( 4.999999999999999112, 7.360373001730986964, -4.729683950898791345 ) ) ;
#12351=EDGE_CURVE ( 'NONE', #2006, #11365, #22209, .T. ) ;
#12352=CARTESIAN_POINT ( 'NONE',  ( 4.999999999999999112, 1.239665997526886665, 9.314797388894895391 ) ) ;
#12356=EDGE_CURVE ( 'NONE', #2402, #14427, #8819, .T. ) ;
#12375=DIRECTION ( 'NONE',  ( 0.000000000000000000, -0.5877852522924802425, 0.8090169943749423442 ) ) ;
#12376=DIRECTION ( 'NONE',  ( 0.000000000000000000, 0.000000000000000000, 1.000000000000000000 ) ) ;
#12378=CARTESIAN_POINT ( 'NONE',  ( 4.999999999999999112, 1.464956435139694646, -10.90201369670496945 ) ) ;
#12379=EDGE_CURVE ( 'NONE', #16373, #13481, #11834, .T. ) ;
#12393=ORIENTED_EDGE ( 'NONE', *, *, #3972, .T. ) ;
#12395=AXIS2_PLACEMENT_3D ( 'NONE', #12065, #13736, #17561 ) ;
#12417=( NAMED_UNIT ( * ) PLANE_ANGLE_UNIT ( ) SI_UNIT ( $, .RADIAN. ) );
#12419=DIRECTION ( 'NONE',  ( -1.000000000000000000, -0.000000000000000000, 0.000000000000000000 ) ) ;
#12420=ORIENTED_EDGE ( 'NONE', *, *, #8932, .F. ) ;
#12422=EDGE_CURVE ( 'NONE', #15525, #12867, #4623, .T. ) ;
#12424=AXIS2_PLACEMENT_3D ( 'NONE', #6914, #8592, #8711 ) ;
#12431=EDGE_CURVE ( 'NONE', #5121, #3084, #20533, .T. ) ;
#12443=CARTESIAN_POINT ( 'NONE',  ( 2.499999999999999556, -10.82112760146734765, -1.975651141462352767 ) ) ;
#12445=DIRECTION ( 'NONE',  ( -1.000000000000000000, 0.000000000000000000, -0.000000000000000000 ) ) ;
#12446=ORIENTED_EDGE ( 'NONE', *, *, #18793, .T. ) ;
#12449=CARTESIAN_POINT ( 'NONE',  ( 0.000000000000000000, -9.241976615262169403, 1.699438267350339871 ) ) ;
#12452=FACE_OUTER_BOUND ( 'NONE', #5053, .T. ) ;
#12459=CIRCLE ( 'NONE', #12072, 4.000000000000002665 ) ;
#12473=DIRECTION ( 'NONE',  ( -1.000000000000000000, -0.000000000000000000, 0.000000000000000000 ) ) ;
#12475=CARTESIAN_POINT ( 'NONE',  ( 4.999999999999999112, -9.314797388894882957, -1.239665997526988139 ) ) ;
#12480=CIRCLE ( 'NONE', #10171, 4.000000000000000888 ) ;
#12490=ORIENTED_EDGE ( 'NONE', *, *, #1794, .F. ) ;
#12492=DIRECTION ( 'NONE',  ( -1.000000000000000000, 0.000000000000000000, -0.000000000000000000 ) ) ;
#12496=DIRECTION ( 'NONE',  ( -1.000000000000000000, 0.000000000000000000, -0.000000000000000000 ) ) ;
#12499=DIRECTION ( 'NONE',  ( 0.000000000000000000, 0.9510565162951545304, -0.3090169943749446757 ) ) ;
#12500=AXIS2_PLACEMENT_3D ( 'NONE', #10653, #3546, #23668 ) ;
#12510=CYLINDRICAL_SURFACE ( 'NONE', #22168, 4.000000000000001776 ) ;
#12527=CARTESIAN_POINT ( 'NONE',  ( 0.000000000000000000, -4.729683950898921907, 7.360373001730902587 ) ) ;
#12538=ORIENTED_EDGE ( 'NONE', *, *, #5455, .F. ) ;
#12540=CARTESIAN_POINT ( 'NONE',  ( 4.999999999999999112, -7.360373001730883935, -4.729683950898952105 ) ) ;
#12545=LINE ( 'NONE', #3527, #3242 ) ;
#12550=CIRCLE ( 'NONE', #16333, 4.000000000000001776 ) ;
#12553=AXIS2_PLACEMENT_3D ( 'NONE', #3644, #18495, #9660 ) ;
#12555=ORIENTED_EDGE ( 'NONE', *, *, #12422, .T. ) ;
#12558=VECTOR ( 'NONE', #5452, 1000.000000000000000 ) ;
#12567=CARTESIAN_POINT ( 'NONE',  ( 2.499999999999999556, -5.222868219166784343, -9.680994141368829631 ) ) ;
#12569=DIRECTION ( 'NONE',  ( -1.000000000000000000, 0.000000000000000000, -0.000000000000000000 ) ) ;
#12586=CARTESIAN_POINT ( 'NONE',  ( 0.000000000000000000, 0.000000000000000000, 0.000000000000000000 ) ) ;
#12594=EDGE_CURVE ( 'NONE', #16416, #12095, #4685, .T. ) ;
#12616=CARTESIAN_POINT ( 'NONE',  ( 5.000000000000000888, 5.400000000000000355, 1.000000000000000000 ) ) ;
#12619=CIRCLE ( 'NONE', #17936, 4.000000000000002665 ) ;
#12628=AXIS2_PLACEMENT_3D ( 'NONE', #12906, #16021, #21966 ) ;
#12644=CIRCLE ( 'NONE', #7662, 8.749000000000002331 ) ;
#12645=VERTEX_POINT ( 'NONE', #6253 ) ;
#12653=DIRECTION ( 'NONE',  ( -1.000000000000000000, -0.000000000000000000, 0.000000000000000000 ) ) ;
#12668=FILL_AREA_STYLE ('',( #1715 ) ) ;
#12669=AXIS2_PLACEMENT_3D ( 'NONE', #20853, #4344, #12145 ) ;
#12675=CARTESIAN_POINT ( 'NONE',  ( 4.999999999999999112, -7.958834565716711218, -7.593217523260670454 ) ) ;
#12697=CARTESIAN_POINT ( 'NONE',  ( 4.999999999999999112, -8.152713396088785203, 3.174628368996045946 ) ) ;
#12710=CARTESIAN_POINT ( 'NONE',  ( 0.000000000000000000, 0.000000000000000000, 0.000000000000000000 ) ) ;
#12731=ORIENTED_EDGE ( 'NONE', *, *, #16288, .T. ) ;
#12737=FILL_AREA_STYLE_COLOUR ( '', #22872 ) ;
#12745=CARTESIAN_POINT ( 'NONE',  ( 4.999999999999999112, 4.472189673936787457, 8.264486777890123648 ) ) ;
#12747=DIRECTION ( 'NONE',  ( -1.000000000000000000, 0.000000000000000000, -0.000000000000000000 ) ) ;
#12748=ORIENTED_EDGE ( 'NONE', *, *, #17282, .F. ) ;
#12757=EDGE_CURVE ( 'NONE', #9212, #16229, #9130, .T. ) ;
#12771=AXIS2_PLACEMENT_3D ( 'NONE', #16056, #14268, #947 ) ;
#12783=EDGE_CURVE ( 'NONE', #20740, #22551, #9013, .T. ) ;
#12784=CYLINDRICAL_SURFACE ( 'NONE', #19413, 11.00000000000000000 ) ;
#12787=LINE ( 'NONE', #3535, #12558 ) ;
#12793=DIRECTION ( 'NONE',  ( -1.000000000000000000, 0.000000000000000000, 0.000000000000000000 ) ) ;
#12800=ORIENTED_EDGE ( 'NONE', *, *, #20920, .T. ) ;
#12802=DIRECTION ( 'NONE',  ( 0.000000000000000000, 0.000000000000000000, -1.000000000000000000 ) ) ;
#12816=DIRECTION ( 'NONE',  ( -1.000000000000000000, -0.000000000000000000, 0.000000000000000000 ) ) ;
#12818=VERTEX_POINT ( 'NONE', #5508 ) ;
#12829=CARTESIAN_POINT ( 'NONE',  ( 4.999999999999999112, -8.264486777890077462, -4.472189673936873611 ) ) ;
#12830=EDGE_LOOP ( 'NONE', ( #8971, #11001, #9178, #11036 ) ) ;
#12834=AXIS2_PLACEMENT_3D ( 'NONE', #2450, #4621, #15777 ) ;
#12843=FILL_AREA_STYLE ('',( #12737 ) ) ;
#12847=CARTESIAN_POINT ( 'NONE',  ( 2.499999999999999556, -9.915734732513254102, 4.762163868918236176 ) ) ;
#12851=ADVANCED_FACE ( 'NONE', ( #5274 ), #3236, .T. ) ;
#12863=EDGE_CURVE ( 'NONE', #9354, #12095, #17637, .T. ) ;
#12867=VERTEX_POINT ( 'NONE', #12616 ) ;
#12883=DIRECTION ( 'NONE',  ( 1.000000000000000000, 0.000000000000000000, 0.000000000000000000 ) ) ;
#12892=DIRECTION ( 'NONE',  ( -1.000000000000000000, 0.000000000000000000, 0.000000000000000000 ) ) ;
#12893=FACE_OUTER_BOUND ( 'NONE', #13100, .T. ) ;
#12900=CARTESIAN_POINT ( 'NONE',  ( 4.999999999999999112, -6.772677083992425295, 5.538577986808878251 ) ) ;
#12901=CARTESIAN_POINT ( 'NONE',  ( 4.999999999999999112, -8.734705317681630277, 0.4999240074894146790 ) ) ;
#12906=CARTESIAN_POINT ( 'NONE',  ( 0.000000000000000000, 4.472189673936787457, 8.264486777890123648 ) ) ;
#12911=DIRECTION ( 'NONE',  ( 0.000000000000000000, 0.000000000000000000, 1.000000000000000000 ) ) ;
#12913=EDGE_CURVE ( 'NONE', #4647, #2825, #16097, .T. ) ;
#12915=EDGE_CURVE ( 'NONE', #7761, #1719, #17239, .T. ) ;
#12920=CARTESIAN_POINT ( 'NONE',  ( -20.00005080000000035, 7.347880794884120722E-16, 6.000000000000000888 ) ) ;
#12932=FACE_OUTER_BOUND ( 'NONE', #18080, .T. ) ;
#12958=CYLINDRICAL_SURFACE ( 'NONE', #20669, 4.000000000000000000 ) ;
#12960=VECTOR ( 'NONE', #17186, 1000.000000000000000 ) ;
#12964=SURFACE_STYLE_FILL_AREA ( #12843 ) ;
#12973=DIRECTION ( 'NONE',  ( -1.000000000000000000, -0.000000000000000000, -0.000000000000000000 ) ) ;
#12983=CIRCLE ( 'NONE', #11464, 11.00000000000000000 ) ;
#12985=ORIENTED_EDGE ( 'NONE', *, *, #8449, .F. ) ;
#12990=EDGE_CURVE ( 'NONE', #21998, #872, #5377, .T. ) ;
#13023=CIRCLE ( 'NONE', #3441, 8.749000000000002331 ) ;
#13031=CARTESIAN_POINT ( 'NONE',  ( 2.499999999999999556, 10.90201369670498721, 1.464956435139581403 ) ) ;
#13033=FACE_OUTER_BOUND ( 'NONE', #18114, .T. ) ;
#13034=EDGE_LOOP ( 'NONE', ( #20292, #15632, #960, #5615 ) ) ;
#13039=ORIENTED_EDGE ( 'NONE', *, *, #17410, .F. ) ;
#13041=ADVANCED_FACE ( 'NONE', ( #584 ), #12958, .F. ) ;
#13050=ADVANCED_FACE ( 'NONE', ( #2264 ), #2383, .T. ) ;
#13055=ORIENTED_EDGE ( 'NONE', *, *, #7745, .T. ) ;
#13065=ORIENTED_EDGE ( 'NONE', *, *, #5867, .F. ) ;
#13066=CARTESIAN_POINT ( 'NONE',  ( 0.000000000000000000, 5.538577986808900455, 6.772677083992405755 ) ) ;
#13070=DIRECTION ( 'NONE',  ( -1.000000000000000000, 0.000000000000000000, -0.000000000000000000 ) ) ;
#13071=DIRECTION ( 'NONE',  ( -1.000000000000000000, -0.000000000000000000, -0.000000000000000000 ) ) ;
#13075=CARTESIAN_POINT ( 'NONE',  ( 0.000000000000000000, -7.593217523260641144, 7.958834565716742304 ) ) ;
#13083=EDGE_CURVE ( 'NONE', #16416, #16674, #10764, .T. ) ;
#13100=EDGE_LOOP ( 'NONE', ( #23536, #22008, #20094, #20414 ) ) ;
#13115=CARTESIAN_POINT ( 'NONE',  ( 4.999999999999999112, -6.807171995660539210, -6.478011392632959442 ) ) ;
#13129=DIRECTION ( 'NONE',  ( 0.000000000000000000, 0.000000000000000000, 1.000000000000000000 ) ) ;
#13134=ORIENTED_EDGE ( 'NONE', *, *, #3794, .F. ) ;
#13146=CARTESIAN_POINT ( 'NONE',  ( -10.00000000000000000, 0.000000000000000000, 0.000000000000000000 ) ) ;
#13154=EDGE_CURVE ( 'NONE', #2890, #14518, #6155, .T. ) ;
#13167=CARTESIAN_POINT ( 'NONE',  ( 4.999999999999999112, -0.4999240074893842034, -8.734705317681632053 ) ) ;
#13170=FACE_OUTER_BOUND ( 'NONE', #19174, .T. ) ;
#13171=FACE_OUTER_BOUND ( 'NONE', #9599, .T. ) ;
#13179=CARTESIAN_POINT ( 'NONE',  ( -10.00000000000000000, 0.000000000000000000, 0.000000000000000000 ) ) ;
#13185=EDGE_CURVE ( 'NONE', #8728, #17247, #17690, .T. ) ;
#13187=ORIENTED_EDGE ( 'NONE', *, *, #14094, .F. ) ;
#13199=EDGE_CURVE ( 'NONE', #8748, #3547, #3537, .T. ) ;
#13203=DIRECTION ( 'NONE',  ( -1.000000000000000000, -0.000000000000000000, -0.000000000000000000 ) ) ;
#13206=EDGE_CURVE ( 'NONE', #21976, #6753, #1419, .T. ) ;
#13207=DIRECTION ( 'NONE',  ( 0.000000000000000000, 0.000000000000000000, 1.000000000000000000 ) ) ;
#13253=ORIENTED_EDGE ( 'NONE', *, *, #3924, .F. ) ;
#13265=CARTESIAN_POINT ( 'NONE',  ( 0.000000000000000000, 8.264486777890107660, 4.472189673936815879 ) ) ;
#13270=CARTESIAN_POINT ( 'NONE',  ( 0.000000000000000000, 9.680994141368771011, 5.222868219166890036 ) ) ;
#13273=DIRECTION ( 'NONE',  ( -1.000000000000000000, -0.000000000000000000, -0.000000000000000000 ) ) ;
#13275=ORIENTED_EDGE ( 'NONE', *, *, #3074, .F. ) ;
#13282=ORIENTED_EDGE ( 'NONE', *, *, #14094, .T. ) ;
#13284=EDGE_LOOP ( 'NONE', ( #5392, #22451, #16776, #17005 ) ) ;
#13289=DIRECTION ( 'NONE',  ( 1.000000000000000000, 0.000000000000000000, 0.000000000000000000 ) ) ;
#13295=DIRECTION ( 'NONE',  ( 0.000000000000000000, -0.8090169943749532244, 0.5877852522924652545 ) ) ;
#13302=ORIENTED_EDGE ( 'NONE', *, *, #9725, .T. ) ;
#13308=AXIS2_PLACEMENT_3D ( 'NONE', #8590, #14105, #12318 ) ;
#13309=EDGE_CURVE ( 'NONE', #7048, #16373, #10638, .T. ) ;
#13311=ADVANCED_FACE ( 'NONE', ( #2327 ), #18613, .T. ) ;
#13315=AXIS2_PLACEMENT_3D ( 'NONE', #8951, #19573, #17683 ) ;
#13336=DIRECTION ( 'NONE',  ( -1.000000000000000000, -0.000000000000000000, -0.000000000000000000 ) ) ;
#13348=DIRECTION ( 'NONE',  ( 0.000000000000000000, 0.000000000000000000, 1.000000000000000000 ) ) ;
#13358=ORIENTED_EDGE ( 'NONE', *, *, #2436, .F. ) ;
#13364=LINE ( 'NONE', #11577, #5570 ) ;
#13367=CIRCLE ( 'NONE', #23661, 11.00000000000000000 ) ;
#13373=CIRCLE ( 'NONE', #19830, 4.000000000000001776 ) ;
#13391=LINE ( 'NONE', #16720, #1734 ) ;
#13397=EDGE_LOOP ( 'NONE', ( #2931, #4535, #10240, #13302 ) ) ;
#13401=ORIENTED_EDGE ( 'NONE', *, *, #18037, .T. ) ;
#13410=DIRECTION ( 'NONE',  ( -1.000000000000000000, 0.000000000000000000, -0.000000000000000000 ) ) ;
#13415=DIRECTION ( 'NONE',  ( 1.000000000000000000, 0.000000000000000000, -0.000000000000000000 ) ) ;
#13417=DIRECTION ( 'NONE',  ( 1.000000000000000000, -0.000000000000000000, -0.000000000000000000 ) ) ;
#13420=VERTEX_POINT ( 'NONE', #20987 ) ;
#13427=DIRECTION ( 'NONE',  ( 0.000000000000000000, -0.8090169943749532244, 0.5877852522924653655 ) ) ;
#13429=CARTESIAN_POINT ( 'NONE',  ( 0.000000000000000000, -8.461683424509299556, -2.223716399045660097 ) ) ;
#13436=CARTESIAN_POINT ( 'NONE',  ( -10.00000000000000000, 0.000000000000000000, 0.000000000000000000 ) ) ;
#13444=LINE ( 'NONE', #22859, #8020 ) ;
#13460=ORIENTED_EDGE ( 'NONE', *, *, #1455, .T. ) ;
#13473=DIRECTION ( 'NONE',  ( 0.000000000000000000, 0.000000000000000000, 1.000000000000000000 ) ) ;
#13481=VERTEX_POINT ( 'NONE', #12527 ) ;
#13525=CYLINDRICAL_SURFACE ( 'NONE', #23523, 4.000000000000000888 ) ;
#13530=CARTESIAN_POINT ( 'NONE',  ( 4.999999999999999112, 0.000000000000000000, 0.000000000000000000 ) ) ;
#13532=AXIS2_PLACEMENT_3D ( 'NONE', #10257, #1116, #21340 ) ;
#13539=ORIENTED_EDGE ( 'NONE', *, *, #17706, .T. ) ;
#13545=AXIS2_PLACEMENT_3D ( 'NONE', #10526, #4993, #2938 ) ;
#13550=VECTOR ( 'NONE', #9197, 1000.000000000000000 ) ;
#13555=CYLINDRICAL_SURFACE ( 'NONE', #8232, 4.000000000000000000 ) ;
#13559=CARTESIAN_POINT ( 'NONE',  ( 4.999999999999999112, 0.000000000000000000, 8.749000000000002331 ) ) ;
#13561=CARTESIAN_POINT ( 'NONE',  ( 4.999999999999999112, 0.000000000000000000, 0.000000000000000000 ) ) ;
#13568=DIRECTION ( 'NONE',  ( 0.000000000000000000, 0.000000000000000000, -1.000000000000000000 ) ) ;
#13569=ORIENTED_EDGE ( 'NONE', *, *, #19710, .T. ) ;
#13601=ORIENTED_EDGE ( 'NONE', *, *, #9801, .F. ) ;
#13602=DIRECTION ( 'NONE',  ( -1.000000000000000000, -0.000000000000000000, 0.000000000000000000 ) ) ;
#13607=EDGE_CURVE ( 'NONE', #11847, #7761, #11782, .T. ) ;
#13616=ADVANCED_FACE ( 'NONE', ( #17664 ), #21455, .T. ) ;
#13620=CARTESIAN_POINT ( 'NONE',  ( 4.999999999999999112, 9.314797388894893615, 1.239665997526919083 ) ) ;
#13626=AXIS2_PLACEMENT_3D ( 'NONE', #11742, #19244, #20799 ) ;
#13627=DIRECTION ( 'NONE',  ( 0.000000000000000000, 0.000000000000000000, 1.000000000000000000 ) ) ;
#13631=EDGE_CURVE ( 'NONE', #22338, #2643, #3148, .T. ) ;
#13646=CYLINDRICAL_SURFACE ( 'NONE', #17223, 8.749000000000002331 ) ;
#13668=DIRECTION ( 'NONE',  ( -1.000000000000000000, 0.000000000000000000, 0.000000000000000000 ) ) ;
#13679=CARTESIAN_POINT ( 'NONE',  ( 4.999999999999999112, 0.000000000000000000, 0.000000000000000000 ) ) ;
#13682=ORIENTED_EDGE ( 'NONE', *, *, #13943, .T. ) ;
#13685=ORIENTED_EDGE ( 'NONE', *, *, #15382, .F. ) ;
#13705=AXIS2_PLACEMENT_3D ( 'NONE', #19931, #19689, #1366 ) ;
#13707=ORIENTED_EDGE ( 'NONE', *, *, #3069, .F. ) ;
#13714=DIRECTION ( 'NONE',  ( -1.000000000000000000, 0.000000000000000000, 0.000000000000000000 ) ) ;
#13718=DIRECTION ( 'NONE',  ( 0.000000000000000000, -0.5877852522924801315, 0.8090169943749423442 ) ) ;
#13725=CARTESIAN_POINT ( 'NONE',  ( 4.999999999999999112, 8.475820894093034852, -4.057423117305300586 ) ) ;
#13730=CARTESIAN_POINT ( 'NONE',  ( 4.999999999999999112, 4.472189673936902921, -8.264486777890061475 ) ) ;
#13736=DIRECTION ( 'NONE',  ( 1.000000000000000000, 0.000000000000000000, 0.000000000000000000 ) ) ;
#13737=DIRECTION ( 'NONE',  ( 0.000000000000000000, -0.3090169943749350168, -0.9510565162951576390 ) ) ;
#13746=VECTOR ( 'NONE', #7524, 1000.000000000000000 ) ;
#13747=EDGE_CURVE ( 'NONE', #18227, #22338, #6427, .T. ) ;
#13769=CARTESIAN_POINT ( 'NONE',  ( 4.999999999999999112, 0.000000000000000000, 0.000000000000000000 ) ) ;
#13771=CARTESIAN_POINT ( 'NONE',  ( 0.000000000000000000, 8.152713396088763886, 3.174628368996105010 ) ) ;
#13779=EDGE_CURVE ( 'NONE', #7617, #22160, #20923, .T. ) ;
#13781=ORIENTED_EDGE ( 'NONE', *, *, #11696, .T. ) ;
#13783=EDGE_LOOP ( 'NONE', ( #8442, #2777, #9678, #4348 ) ) ;
#13786=EDGE_CURVE ( 'NONE', #15640, #9577, #19789, .T. ) ;
#13792=ORIENTED_EDGE ( 'NONE', *, *, #21493, .F. ) ;
#13800=CARTESIAN_POINT ( 'NONE',  ( 0.000000000000000000, 0.000000000000000000, 0.000000000000000000 ) ) ;
#13806=DIRECTION ( 'NONE',  ( 0.000000000000000000, 0.000000000000000000, 1.000000000000000000 ) ) ;
#13813=ORIENTED_EDGE ( 'NONE', *, *, #241, .F. ) ;
#13821=CARTESIAN_POINT ( 'NONE',  ( 4.999999999999999112, -7.360373001730883935, -4.729683950898952105 ) ) ;
#13829=DIRECTION ( 'NONE',  ( 0.000000000000000000, 0.000000000000000000, 1.000000000000000000 ) ) ;
#13832=LINE ( 'NONE', #16321, #3450 ) ;
#13833=CIRCLE ( 'NONE', #15749, 11.00000000000000000 ) ;
#13834=ORIENTED_EDGE ( 'NONE', *, *, #23599, .T. ) ;
#13843=CARTESIAN_POINT ( 'NONE',  ( 4.999999999999999112, -8.461683424509331530, 2.223716399045538861 ) ) ;
#13860=ORIENTED_EDGE ( 'NONE', *, *, #23533, .T. ) ;
#13866=ORIENTED_EDGE ( 'NONE', *, *, #17844, .F. ) ;
#13886=FACE_OUTER_BOUND ( 'NONE', #1448, .T. ) ;
#13891=CARTESIAN_POINT ( 'NONE',  ( 4.999999999999999112, -7.360373001730951437, 4.729683950898845524 ) ) ;
#13893=ORIENTED_EDGE ( 'NONE', *, *, #13631, .F. ) ;
#13903=EDGE_CURVE ( 'NONE', #7993, #3902, #1816, .T. ) ;
#13905=EDGE_CURVE ( 'NONE', #15228, #17794, #8512, .T. ) ;
#13914=AXIS2_PLACEMENT_3D ( 'NONE', #10211, #8408, #9975 ) ;
#13915=DIRECTION ( 'NONE',  ( -1.000000000000000000, 0.000000000000000000, 0.000000000000000000 ) ) ;
#13925=DIRECTION ( 'NONE',  ( -1.000000000000000000, -0.000000000000000000, -0.000000000000000000 ) ) ;
#13943=EDGE_CURVE ( 'NONE', #2142, #15640, #16371, .T. ) ;
#13953=ORIENTED_EDGE ( 'NONE', *, *, #316, .F. ) ;
#13972=DIRECTION ( 'NONE',  ( -1.000000000000000000, 0.000000000000000000, 0.000000000000000000 ) ) ;
#13974=ORIENTED_EDGE ( 'NONE', *, *, #12990, .F. ) ;
#13980=ORIENTED_EDGE ( 'NONE', *, *, #12915, .F. ) ;
#13982=ORIENTED_EDGE ( 'NONE', *, *, #3205, .T. ) ;
#13995=CARTESIAN_POINT ( 'NONE',  ( -20.00005080000000035, 0.000000000000000000, -6.000000000000000888 ) ) ;
#14000=CARTESIAN_POINT ( 'NONE',  ( 2.499999999999999556, 9.680994141368849171, -5.222868219166749704 ) ) ;
#14001=DIRECTION ( 'NONE',  ( 0.000000000000000000, 0.000000000000000000, 1.000000000000000000 ) ) ;
#14003=AXIS2_PLACEMENT_3D ( 'NONE', #5463, #1263, #8717 ) ;
#14020=DIRECTION ( 'NONE',  ( -1.000000000000000000, 0.000000000000000000, 0.000000000000000000 ) ) ;
#14055=EDGE_CURVE ( 'NONE', #18107, #12101, #8734, .T. ) ;
#14060=DIRECTION ( 'NONE',  ( 0.000000000000000000, -0.9510565162951565288, 0.3090169943749382364 ) ) ;
#14062=EDGE_CURVE ( 'NONE', #16322, #5065, #8867, .T. ) ;
#14063=VERTEX_POINT ( 'NONE', #1760 ) ;
#14069=EDGE_CURVE ( 'NONE', #5065, #5121, #9127, .T. ) ;
#14070=CARTESIAN_POINT ( 'NONE',  ( -10.00000000000000000, 0.000000000000000000, 0.000000000000000000 ) ) ;
#14079=CARTESIAN_POINT ( 'NONE',  ( 4.999999999999999112, -1.239665997526817165, -9.314797388894906049 ) ) ;
#14085=DIRECTION ( 'NONE',  ( 0.000000000000000000, 0.000000000000000000, 1.000000000000000000 ) ) ;
#14093=AXIS2_PLACEMENT_3D ( 'NONE', #4254, #15529, #22677 ) ;
#14094=EDGE_CURVE ( 'NONE', #7617, #15752, #5126, .T. ) ;
#14095=CARTESIAN_POINT ( 'NONE',  ( 4.999999999999999112, 8.264486777890107660, -4.472189673936815879 ) ) ;
#14096=EDGE_LOOP ( 'NONE', ( #19160, #18871, #6669, #6699 ) ) ;
#14105=DIRECTION ( 'NONE',  ( -1.000000000000000000, 0.000000000000000000, 0.000000000000000000 ) ) ;
#14119=VECTOR ( 'NONE', #23444, 1000.000000000000000 ) ;
#14151=ORIENTED_EDGE ( 'NONE', *, *, #11629, .T. ) ;
#14158=DIRECTION ( 'NONE',  ( -1.000000000000000000, -0.000000000000000000, 0.000000000000000000 ) ) ;
#14161=ORIENTED_EDGE ( 'NONE', *, *, #15533, .T. ) ;
#14163=AXIS2_PLACEMENT_3D ( 'NONE', #16505, #83, #7416 ) ;
#14165=AXIS2_PLACEMENT_3D ( 'NONE', #12085, #19349, #10415 ) ;
#14167=CARTESIAN_POINT ( 'NONE',  ( 4.999999999999999112, -4.057423117305329896, -8.475820894093020641 ) ) ;
#14175=CARTESIAN_POINT ( 'NONE',  ( 4.999999999999999112, -4.472189673936728838, -8.264486777890155622 ) ) ;
#14179=AXIS2_PLACEMENT_3D ( 'NONE', #5600, #10553, #17827 ) ;
#14180=ORIENTED_EDGE ( 'NONE', *, *, #17253, .T. ) ;
#14186=ADVANCED_FACE ( 'NONE', ( #8215 ), #22568, .T. ) ;
#14187=DIRECTION ( 'NONE',  ( -1.000000000000000000, -0.000000000000000000, 0.000000000000000000 ) ) ;
#14188=ORIENTED_EDGE ( 'NONE', *, *, #11460, .F. ) ;
#14190=DIRECTION ( 'NONE',  ( 0.000000000000000000, -0.9510565162951565288, 0.3090169943749382364 ) ) ;
#14204=EDGE_CURVE ( 'NONE', #22615, #11403, #5271, .T. ) ;
#14224=EDGE_LOOP ( 'NONE', ( #15315, #13253, #13358, #16798 ) ) ;
#14240=ORIENTED_EDGE ( 'NONE', *, *, #23411, .F. ) ;
#14241=CARTESIAN_POINT ( 'NONE',  ( 0.000000000000000000, -8.734705317681630277, 0.4999240074894146790 ) ) ;
#14244=EDGE_CURVE ( 'NONE', #20275, #3528, #7972, .T. ) ;
#14246=ORIENTED_EDGE ( 'NONE', *, *, #4401, .T. ) ;
#14247=CARTESIAN_POINT ( 'NONE',  ( 4.999999999999999112, 1.239665997527020558, -9.314797388894877628 ) ) ;
#14250=ORIENTED_EDGE ( 'NONE', *, *, #18614, .T. ) ;
#14257=DIRECTION ( 'NONE',  ( -1.000000000000000000, -0.000000000000000000, -0.000000000000000000 ) ) ;
#14265=CARTESIAN_POINT ( 'NONE',  ( 0.000000000000000000, 6.772677083992387992, 5.538577986808924436 ) ) ;
#14268=DIRECTION ( 'NONE',  ( 1.000000000000000000, -0.000000000000000000, -0.000000000000000000 ) ) ;
#14276=CARTESIAN_POINT ( 'NONE',  ( 0.000000000000000000, 2.223716399045570835, 8.461683424509324425 ) ) ;
#14279=ORIENTED_EDGE ( 'NONE', *, *, #18463, .T. ) ;
#14280=LINE ( 'NONE', #23593, #14471 ) ;
#14283=CARTESIAN_POINT ( 'NONE',  ( 0.000000000000000000, 0.000000000000000000, 0.000000000000000000 ) ) ;
#14284=PLANE ( 'NONE',  #737 ) ;
#14295=FACE_OUTER_BOUND ( 'NONE', #14834, .T. ) ;
#14296=ORIENTED_EDGE ( 'NONE', *, *, #10631, .T. ) ;
#14298=VERTEX_POINT ( 'NONE', #16068 ) ;
#14304=DIRECTION ( 'NONE',  ( -1.000000000000000000, 0.000000000000000000, 0.000000000000000000 ) ) ;
#14309=ORIENTED_EDGE ( 'NONE', *, *, #3762, .T. ) ;
#14313=DIRECTION ( 'NONE',  ( -1.000000000000000000, -0.000000000000000000, 0.000000000000000000 ) ) ;
#14317=CARTESIAN_POINT ( 'NONE',  ( 4.999999999999999112, 7.360373001730920350, 4.729683950898897926 ) ) ;
#14338=DIRECTION ( 'NONE',  ( -1.000000000000000000, -0.000000000000000000, -0.000000000000000000 ) ) ;
#14340=EDGE_CURVE ( 'NONE', #6517, #4629, #14280, .T. ) ;
#14345=AXIS2_PLACEMENT_3D ( 'NONE', #22350, #13289, #23306 ) ;
#14348=AXIS2_PLACEMENT_3D ( 'NONE', #9404, #16578, #5438 ) ;
#14359=CARTESIAN_POINT ( 'NONE',  ( 4.999999999999999112, 10.82112760146739205, -1.975651141462126059 ) ) ;
#14360=ORIENTED_EDGE ( 'NONE', *, *, #21487, .T. ) ;
#14361=DIRECTION ( 'NONE',  ( -1.000000000000000000, 0.000000000000000000, -0.000000000000000000 ) ) ;
#14368=AXIS2_PLACEMENT_3D ( 'NONE', #18200, #2253, #18541 ) ;
#14374=DIRECTION ( 'NONE',  ( 1.000000000000000000, 0.000000000000000000, 0.000000000000000000 ) ) ;
#14376=CARTESIAN_POINT ( 'NONE',  ( 2.499999999999999556, -9.680994141368808314, 5.222868219166821646 ) ) ;
#14380=CARTESIAN_POINT ( 'NONE',  ( 0.000000000000000000, -2.223716399045513548, -8.461683424509336859 ) ) ;
#14397=AXIS2_PLACEMENT_3D ( 'NONE', #20692, #8259, #8024 ) ;
#14398=AXIS2_PLACEMENT_3D ( 'NONE', #19040, #13915, #8284 ) ;
#14406=EDGE_CURVE ( 'NONE', #5525, #19779, #1905, .T. ) ;
#14415=CARTESIAN_POINT ( 'NONE',  ( 4.999999999999999112, 5.538577986808900455, 6.772677083992405755 ) ) ;
#14418=ORIENTED_EDGE ( 'NONE', *, *, #14244, .F. ) ;
#14426=FACE_OUTER_BOUND ( 'NONE', #8765, .T. ) ;
#14427=VERTEX_POINT ( 'NONE', #9248 ) ;
#14436=FACE_OUTER_BOUND ( 'NONE', #14848, .T. ) ;
#14444=DIRECTION ( 'NONE',  ( -1.000000000000000000, 0.000000000000000000, 0.000000000000000000 ) ) ;
#14455=ORIENTED_EDGE ( 'NONE', *, *, #14953, .F. ) ;
#14458=CYLINDRICAL_SURFACE ( 'NONE', #21280, 4.000000000000001776 ) ;
#14461=AXIS2_PLACEMENT_3D ( 'NONE', #1864, #11488, #5708 ) ;
#14471=VECTOR ( 'NONE', #12492, 1000.000000000000000 ) ;
#14473=CARTESIAN_POINT ( 'NONE',  ( 4.999999999999999112, 6.772677083992466152, -5.538577986808826736 ) ) ;
#14474=ORIENTED_EDGE ( 'NONE', *, *, #3972, .F. ) ;
#14482=DIRECTION ( 'NONE',  ( 0.000000000000000000, 0.5877852522924743583, -0.8090169943749467851 ) ) ;
#14483=ORIENTED_EDGE ( 'NONE', *, *, #13786, .T. ) ;
#14495=CARTESIAN_POINT ( 'NONE',  ( 0.000000000000000000, 7.360373001730986964, -4.729683950898791345 ) ) ;
#14503=DIRECTION ( 'NONE',  ( -1.000000000000000000, 0.000000000000000000, -0.000000000000000000 ) ) ;
#14506=ORIENTED_EDGE ( 'NONE', *, *, #21493, .T. ) ;
#14513=CIRCLE ( 'NONE', #17559, 8.749000000000002331 ) ;
#14518=VERTEX_POINT ( 'NONE', #18548 ) ;
#14530=CIRCLE ( 'NONE', #3020, 4.000000000000001776 ) ;
#14554=VERTEX_POINT ( 'NONE', #21043 ) ;
#14563=CYLINDRICAL_SURFACE ( 'NONE', #19390, 4.000000000000001776 ) ;
#14572=VERTEX_POINT ( 'NONE', #8031 ) ;
#14583=DIRECTION ( 'NONE',  ( 0.000000000000000000, 0.000000000000000000, 1.000000000000000000 ) ) ;
#14587=DIRECTION ( 'NONE',  ( -1.000000000000000000, 0.000000000000000000, 0.000000000000000000 ) ) ;
#14603=DIRECTION ( 'NONE',  ( 0.000000000000000000, 0.000000000000000000, 1.000000000000000000 ) ) ;
#14604=ORIENTED_EDGE ( 'NONE', *, *, #2891, .T. ) ;
#14613=DIRECTION ( 'NONE',  ( -1.000000000000000000, 0.000000000000000000, 0.000000000000000000 ) ) ;
#14620=ADVANCED_FACE ( 'NONE', ( #820 ), #15463, .T. ) ;
#14634=CARTESIAN_POINT ( 'NONE',  ( 4.999999999999999112, -9.314797388894900720, 1.239665997526853580 ) ) ;
#14635=ORIENTED_EDGE ( 'NONE', *, *, #21550, .T. ) ;
#14647=LINE ( 'NONE', #12847, #9175 ) ;
#14674=EDGE_CURVE ( 'NONE', #5335, #21100, #19062, .T. ) ;
#14691=ORIENTED_EDGE ( 'NONE', *, *, #16566, .T. ) ;
#14702=EDGE_CURVE ( 'NONE', #6515, #17055, #8362, .T. ) ;
#14705=DIRECTION ( 'NONE',  ( -1.000000000000000000, 0.000000000000000000, -0.000000000000000000 ) ) ;
#14709=DIRECTION ( 'NONE',  ( 0.000000000000000000, 0.000000000000000000, 1.000000000000000000 ) ) ;
#14712=ORIENTED_EDGE ( 'NONE', *, *, #11617, .F. ) ;
#14714=CARTESIAN_POINT ( 'NONE',  ( -10.00000000000000000, 0.000000000000000000, 0.000000000000000000 ) ) ;
#14716=VERTEX_POINT ( 'NONE', #7445 ) ;
#14718=ORIENTED_EDGE ( 'NONE', *, *, #1145, .T. ) ;
#14725=MANIFOLD_SOLID_BREP ( 'Keyway', #1262 ) ;
#14726=AXIS2_PLACEMENT_3D ( 'NONE', #15335, #1034, #15449 ) ;
#14738=ORIENTED_EDGE ( 'NONE', *, *, #1017, .F. ) ;
#14741=DIRECTION ( 'NONE',  ( 0.000000000000000000, 0.000000000000000000, 1.000000000000000000 ) ) ;
#14763=AXIS2_PLACEMENT_3D ( 'NONE', #22237, #20438, #4047 ) ;
#14776=EDGE_LOOP ( 'NONE', ( #762, #10886, #22494, #20781 ) ) ;
#14783=ORIENTED_EDGE ( 'NONE', *, *, #3205, .F. ) ;
#14821=DIRECTION ( 'NONE',  ( 0.000000000000000000, -6.982962677686266711E-15, 1.000000000000000000 ) ) ;
#14826=DIRECTION ( 'NONE',  ( 1.000000000000000000, 0.000000000000000000, 0.000000000000000000 ) ) ;
#14829=CARTESIAN_POINT ( 'NONE',  ( 0.000000000000000000, -1.699438267350438903, 9.241976615262153416 ) ) ;
#14832=DIRECTION ( 'NONE',  ( -1.000000000000000000, 0.000000000000000000, 0.000000000000000000 ) ) ;
#14833=ORIENTED_EDGE ( 'NONE', *, *, #316, .T. ) ;
#14834=EDGE_LOOP ( 'NONE', ( #1548, #16696, #22835, #15557 ) ) ;
#14838=VERTEX_POINT ( 'NONE', #14495 ) ;
#14841=AXIS2_PLACEMENT_3D ( 'NONE', #10782, #15912, #5115 ) ;
#14845=VECTOR ( 'NONE', #12653, 1000.000000000000000 ) ;
#14848=EDGE_LOOP ( 'NONE', ( #13866, #7864, #12800, #18031 ) ) ;
#14850=VECTOR ( 'NONE', #23200, 1000.000000000000000 ) ;
#14855=AXIS2_PLACEMENT_3D ( 'NONE', #23440, #9088, #10660 ) ;
#14860=DIRECTION ( 'NONE',  ( -1.000000000000000000, 0.000000000000000000, -0.000000000000000000 ) ) ;
#14876=DIRECTION ( 'NONE',  ( -1.000000000000000000, 0.000000000000000000, -0.000000000000000000 ) ) ;
#14877=CIRCLE ( 'NONE', #12195, 4.000000000000001776 ) ;
#14885=FACE_OUTER_BOUND ( 'NONE', #16642, .T. ) ;
#14889=DIRECTION ( 'NONE',  ( -1.000000000000000000, 0.000000000000000000, 0.000000000000000000 ) ) ;
#14891=CARTESIAN_POINT ( 'NONE',  ( 4.999999999999999112, 0.000000000000000000, 0.000000000000000000 ) ) ;
#14923=AXIS2_PLACEMENT_3D ( 'NONE', #9133, #5, #12499 ) ;
#14926=AXIS2_PLACEMENT_3D ( 'NONE', #10557, #1399, #2851 ) ;
#14928=DIRECTION ( 'NONE',  ( 0.000000000000000000, 0.000000000000000000, -1.000000000000000000 ) ) ;
#14936=DIRECTION ( 'NONE',  ( -1.000000000000000000, -0.000000000000000000, -0.000000000000000000 ) ) ;
#14940=CARTESIAN_POINT ( 'NONE',  ( 4.999999999999999112, 1.699438267350500409, -9.241976615262139205 ) ) ;
#14943=EDGE_CURVE ( 'NONE', #9577, #17502, #13367, .T. ) ;
#14953=EDGE_CURVE ( 'NONE', #22213, #15687, #7057, .T. ) ;
#14957=CYLINDRICAL_SURFACE ( 'NONE', #16679, 11.00000000000000000 ) ;
#14958=ORIENTED_EDGE ( 'NONE', *, *, #3194, .T. ) ;
#14962=ORIENTED_EDGE ( 'NONE', *, *, #14069, .T. ) ;
#14969=AXIS2_PLACEMENT_3D ( 'NONE', #1565, #3599, #9146 ) ;
#14972=EDGE_CURVE ( 'NONE', #9225, #5230, #15286, .T. ) ;
#14993=EDGE_LOOP ( 'NONE', ( #10573, #17391, #20454, #16165 ) ) ;
#14998=ORIENTED_EDGE ( 'NONE', *, *, #23397, .F. ) ;
#15007=ORIENTED_EDGE ( 'NONE', *, *, #6138, .F. ) ;
#15012=LINE ( 'NONE', #20823, #21572 ) ;
#15018=DIRECTION ( 'NONE',  ( 0.000000000000000000, 0.000000000000000000, 1.000000000000000000 ) ) ;
#15025=CARTESIAN_POINT ( 'NONE',  ( 0.000000000000000000, -10.90201369670497655, -1.464956435139657343 ) ) ;
#15049=AXIS2_PLACEMENT_3D ( 'NONE', #5518, #7098, #21804 ) ;
#15062=CARTESIAN_POINT ( 'NONE',  ( 4.999999999999999112, 0.000000000000000000, 0.000000000000000000 ) ) ;
#15064=VECTOR ( 'NONE', #4671, 1000.000000000000000 ) ;
#15067=LINE ( 'NONE', #13031, #9575 ) ;
#15074=ORIENTED_EDGE ( 'NONE', *, *, #4567, .F. ) ;
#15081=LINE ( 'NONE', #22337, #325 ) ;
#15098=CARTESIAN_POINT ( 'NONE',  ( 0.000000000000000000, -6.478011392632939014, 6.807171995660559638 ) ) ;
#15113=DIRECTION ( 'NONE',  ( 0.000000000000000000, 0.000000000000000000, 1.000000000000000000 ) ) ;
#15124=AXIS2_PLACEMENT_3D ( 'NONE', #2778, #19194, #7958 ) ;
#15128=AXIS2_PLACEMENT_3D ( 'NONE', #21800, #7452, #18564 ) ;
#15131=ORIENTED_EDGE ( 'NONE', *, *, #1593, .T. ) ;
#15136=ORIENTED_EDGE ( 'NONE', *, *, #11791, .T. ) ;
#15147=VECTOR ( 'NONE', #13417, 1000.000000000000000 ) ;
#15161=CIRCLE ( 'NONE', #20463, 11.00000000000000000 ) ;
#15164=CIRCLE ( 'NONE', #12500, 4.000000000000001776 ) ;
#15165=CYLINDRICAL_SURFACE ( 'NONE', #18557, 4.000000000000001776 ) ;
#15174=DIRECTION ( 'NONE',  ( 0.000000000000000000, 0.000000000000000000, 1.000000000000000000 ) ) ;
#15178=DIRECTION ( 'NONE',  ( -1.000000000000000000, 0.000000000000000000, -0.000000000000000000 ) ) ;
#15195=FACE_OUTER_BOUND ( 'NONE', #8907, .T. ) ;
#15202=AXIS2_PLACEMENT_3D ( 'NONE', #21469, #21350, #14085 ) ;
#15209=ORIENTED_EDGE ( 'NONE', *, *, #4977, .T. ) ;
#15211=ORIENTED_EDGE ( 'NONE', *, *, #6310, .F. ) ;
#15215=CIRCLE ( 'NONE', #2991, 11.00000000000000000 ) ;
#15218=CARTESIAN_POINT ( 'NONE',  ( 25.00005080000000035, 3.872983346207417021, 1.000000000000000000 ) ) ;
#15219=DIRECTION ( 'NONE',  ( -1.000000000000000000, -0.000000000000000000, -0.000000000000000000 ) ) ;
#15221=ORIENTED_EDGE ( 'NONE', *, *, #2346, .T. ) ;
#15228=VERTEX_POINT ( 'NONE', #10735 ) ;
#15229=DIRECTION ( 'NONE',  ( -1.000000000000000000, 0.000000000000000000, -0.000000000000000000 ) ) ;
#15244=DIRECTION ( 'NONE',  ( 0.000000000000000000, -1.000000000000000000, -1.040834085586083783E-14 ) ) ;
#15245=LINE ( 'NONE', #22513, #5759 ) ;
#15248=VERTEX_POINT ( 'NONE', #5070 ) ;
#15255=CARTESIAN_POINT ( 'NONE',  ( 0.000000000000000000, 0.000000000000000000, 0.000000000000000000 ) ) ;
#15259=EDGE_LOOP ( 'NONE', ( #21448, #2488, #7198, #4561 ) ) ;
#15276=EDGE_CURVE ( 'NONE', #1974, #3346, #22017, .T. ) ;
#15277=ORIENTED_EDGE ( 'NONE', *, *, #1504, .T. ) ;
#15282=AXIS2_PLACEMENT_3D ( 'NONE', #2175, #22411, #13348 ) ;
#15284=ORIENTED_EDGE ( 'NONE', *, *, #9687, .T. ) ;
#15286=CIRCLE ( 'NONE', #7625, 4.000000000000001776 ) ;
#15306=CARTESIAN_POINT ( 'NONE',  ( 4.999999999999999112, 4.729683950898977862, -7.360373001730867060 ) ) ;
#15308=EDGE_CURVE ( 'NONE', #8748, #9405, #2260, .T. ) ;
#15310=ORIENTED_EDGE ( 'NONE', *, *, #551, .F. ) ;
#15315=ORIENTED_EDGE ( 'NONE', *, *, #12159, .T. ) ;
#15329=LINE ( 'NONE', #20432, #10327 ) ;
#15335=CARTESIAN_POINT ( 'NONE',  ( 4.999999999999999112, -4.057423117305452465, 8.475820894092962021 ) ) ;
#15351=DIRECTION ( 'NONE',  ( -1.000000000000000000, 0.000000000000000000, 0.000000000000000000 ) ) ;
#15368=FACE_OUTER_BOUND ( 'NONE', #8195, .T. ) ;
#15371=ORIENTED_EDGE ( 'NONE', *, *, #4977, .F. ) ;
#15377=VERTEX_POINT ( 'NONE', #11535 ) ;
#15380=VECTOR ( 'NONE', #14889, 1000.000000000000000 ) ;
#15382=EDGE_CURVE ( 'NONE', #3756, #14716, #3768, .T. ) ;
#15428=EDGE_LOOP ( 'NONE', ( #4491, #15810, #16386, #5360 ) ) ;
#15440=ADVANCED_FACE ( 'NONE', ( #17132 ), #11283, .T. ) ;
#15444=DIRECTION ( 'NONE',  ( 0.000000000000000000, -0.3090169943749549453, 0.9510565162951511997 ) ) ;
#15446=LINE ( 'NONE', #7776, #4252 ) ;
#15449=DIRECTION ( 'NONE',  ( 0.000000000000000000, 0.000000000000000000, 1.000000000000000000 ) ) ;
#15453=DIRECTION ( 'NONE',  ( 0.000000000000000000, 1.000000000000000000, 3.491481338843133355E-15 ) ) ;
#15458=DIRECTION ( 'NONE',  ( 0.000000000000000000, 0.000000000000000000, 1.000000000000000000 ) ) ;
#15463=CYLINDRICAL_SURFACE ( 'NONE', #6440, 8.749000000000002331 ) ;
#15476=EDGE_CURVE ( 'NONE', #22278, #7710, #14513, .T. ) ;
#15477=DIRECTION ( 'NONE',  ( 0.000000000000000000, 0.000000000000000000, -1.000000000000000000 ) ) ;
#15478=ORIENTED_EDGE ( 'NONE', *, *, #18296, .F. ) ;
#15481=CARTESIAN_POINT ( 'NONE',  ( 0.000000000000000000, -4.472189673936728838, -8.264486777890155622 ) ) ;
#15506=DIRECTION ( 'NONE',  ( -1.000000000000000000, -0.000000000000000000, -0.000000000000000000 ) ) ;
#15510=CARTESIAN_POINT ( 'NONE',  ( 0.000000000000000000, 4.057423117305515525, -8.475820894092930047 ) ) ;
#15517=ORIENTED_EDGE ( 'NONE', *, *, #21132, .F. ) ;
#15521=CIRCLE ( 'NONE', #20824, 4.000000000000000888 ) ;
#15525=VERTEX_POINT ( 'NONE', #477 ) ;
#15529=DIRECTION ( 'NONE',  ( -1.000000000000000000, 0.000000000000000000, 0.000000000000000000 ) ) ;
#15533=EDGE_CURVE ( 'NONE', #9405, #8728, #4172, .T. ) ;
#15535=CYLINDRICAL_SURFACE ( 'NONE', #2294, 8.749000000000002331 ) ;
#15538=CIRCLE ( 'NONE', #12081, 4.000000000000001776 ) ;
#15556=CARTESIAN_POINT ( 'NONE',  ( 4.999999999999999112, -2.223716399045513548, -8.461683424509336859 ) ) ;
#15557=ORIENTED_EDGE ( 'NONE', *, *, #14953, .T. ) ;
#15559=CIRCLE ( 'NONE', #23559, 8.749000000000002331 ) ;
#15569=DIRECTION ( 'NONE',  ( -1.000000000000000000, 0.000000000000000000, 0.000000000000000000 ) ) ;
#15577=ORIENTED_EDGE ( 'NONE', *, *, #13199, .T. ) ;
#15586=CARTESIAN_POINT ( 'NONE',  ( 0.000000000000000000, 0.000000000000000000, 0.000000000000000000 ) ) ;
#15588=CARTESIAN_POINT ( 'NONE',  ( 0.000000000000000000, -1.699438267350307008, -9.241976615262174732 ) ) ;
#15607=AXIS2_PLACEMENT_3D ( 'NONE', #19528, #3485, #12376 ) ;
#15617=AXIS2_PLACEMENT_3D ( 'NONE', #21263, #6934, #23442 ) ;
#15619=DIRECTION ( 'NONE',  ( 1.000000000000000000, 0.000000000000000000, 0.000000000000000000 ) ) ;
#15632=ORIENTED_EDGE ( 'NONE', *, *, #23575, .T. ) ;
#15638=VERTEX_POINT ( 'NONE', #12234 ) ;
#15640=VERTEX_POINT ( 'NONE', #23203 ) ;
#15651=DIRECTION ( 'NONE',  ( -1.000000000000000000, 0.000000000000000000, 0.000000000000000000 ) ) ;
#15653=DIRECTION ( 'NONE',  ( -1.000000000000000000, 0.000000000000000000, -0.000000000000000000 ) ) ;
#15659=ORIENTED_EDGE ( 'NONE', *, *, #21792, .F. ) ;
#15661=DIRECTION ( 'NONE',  ( -1.000000000000000000, 0.000000000000000000, 0.000000000000000000 ) ) ;
#15662=ORIENTED_EDGE ( 'NONE', *, *, #17844, .T. ) ;
#15666=ORIENTED_EDGE ( 'NONE', *, *, #2891, .F. ) ;
#15669=EDGE_LOOP ( 'NONE', ( #5483, #18817, #21040, #16204, #1960, #17453, #17742, #4880, #13569, #8006, #16273, #8520, #3928, #18938, #21003, #13601, #23590, #20602, #20718, #4403, #19255, #9275, #5853, #14962, #17474, #15662, #1213, #15940, #22259, #10659, #18893, #8205, #1303, #9848, #6806, #21028, #15211, #13682, #14483, #21096, #1693, #4970, #436, #567, #23102, #10421, #4793, #23557, #22556, #19952, #2065, #21328, #12490, #14691, #21568, #3997, #17594, #3283, #5323, #20102, #11363, #5591, #638, #16972, #17883, #3788, #10784, #15136, #13460, #23142, #7842, #9937, #2515, #20976, #22307, #17307, #14279, #7540, #19836, #10247, #20305, #14246, #15775, #15131, #19278 ) ) ;
#15677=EDGE_CURVE ( 'NONE', #7761, #14838, #5021, .T. ) ;
#15681=DIRECTION ( 'NONE',  ( -1.000000000000000000, 0.000000000000000000, 0.000000000000000000 ) ) ;
#15685=FACE_BOUND ( 'NONE', #9916, .T. ) ;
#15686=DIRECTION ( 'NONE',  ( 0.000000000000000000, 0.000000000000000000, -1.000000000000000000 ) ) ;
#15687=VERTEX_POINT ( 'NONE', #19613 ) ;
#15691=DIRECTION ( 'NONE',  ( 0.000000000000000000, 0.9510565162951544194, -0.3090169943749447312 ) ) ;
#15696=EDGE_CURVE ( 'NONE', #6665, #462, #16053, .T. ) ;
#15718=CYLINDRICAL_SURFACE ( 'NONE', #9631, 6.000000000000000888 ) ;
#15736=AXIS2_PLACEMENT_3D ( 'NONE', #18439, #226, #22134 ) ;
#15743=DIRECTION ( 'NONE',  ( 0.000000000000000000, 0.000000000000000000, 1.000000000000000000 ) ) ;
#15749=AXIS2_PLACEMENT_3D ( 'NONE', #6118, #20825, #11889 ) ;
#15752=VERTEX_POINT ( 'NONE', #14380 ) ;
#15756=CARTESIAN_POINT ( 'NONE',  ( 0.000000000000000000, 0.000000000000000000, 0.000000000000000000 ) ) ;
#15775=ORIENTED_EDGE ( 'NONE', *, *, #16541, .F. ) ;
#15776=DIRECTION ( 'NONE',  ( -1.000000000000000000, 0.000000000000000000, -0.000000000000000000 ) ) ;
#15777=DIRECTION ( 'NONE',  ( 0.000000000000000000, 0.000000000000000000, 1.000000000000000000 ) ) ;
#15797=EDGE_CURVE ( 'NONE', #22762, #5267, #16166, .T. ) ;
#15809=CARTESIAN_POINT ( 'NONE',  ( 4.999999999999999112, 0.000000000000000000, 8.749000000000002331 ) ) ;
#15810=ORIENTED_EDGE ( 'NONE', *, *, #13185, .F. ) ;
#15820=CARTESIAN_POINT ( 'NONE',  ( 4.999999999999999112, -7.593217523260522128, -7.958834565716849774 ) ) ;
#15837=DIRECTION ( 'NONE',  ( 0.000000000000000000, 0.000000000000000000, 1.000000000000000000 ) ) ;
#15842=CARTESIAN_POINT ( 'NONE',  ( 4.999999999999999112, -8.734705317681630277, 0.4999240074894146790 ) ) ;
#15848=CARTESIAN_POINT ( 'NONE',  ( 4.999999999999999112, -8.461683424509297780, -2.223716399045659653 ) ) ;
#15855=ORIENTED_EDGE ( 'NONE', *, *, #22949, .F. ) ;
#15860=EDGE_CURVE ( 'NONE', #3084, #11384, #14530, .T. ) ;
#15867=DIRECTION ( 'NONE',  ( -1.000000000000000000, 0.000000000000000000, 0.000000000000000000 ) ) ;
#15881=ORIENTED_EDGE ( 'NONE', *, *, #10595, .T. ) ;
#15883=PLANE ( 'NONE',  #7453 ) ;
#15887=AXIS2_PLACEMENT_3D ( 'NONE', #22914, #3572, #23456 ) ;
#15888=ADVANCED_FACE ( 'NONE', ( #12932 ), #22105, .T. ) ;
#15901=DIRECTION ( 'NONE',  ( 0.000000000000000000, 0.000000000000000000, 1.000000000000000000 ) ) ;
#15907=EDGE_LOOP ( 'NONE', ( #11272, #21142, #11281, #3552 ) ) ;
#15912=DIRECTION ( 'NONE',  ( -1.000000000000000000, 0.000000000000000000, 0.000000000000000000 ) ) ;
#15917=ORIENTED_EDGE ( 'NONE', *, *, #6735, .T. ) ;
#15940=ORIENTED_EDGE ( 'NONE', *, *, #20757, .T. ) ;
#15949=EDGE_CURVE ( 'NONE', #8014, #11236, #15329, .T. ) ;
#15957=CIRCLE ( 'NONE', #15202, 4.000000000000000000 ) ;
#15959=DIRECTION ( 'NONE',  ( 0.000000000000000000, 0.5877852522924742473, -0.8090169943749466741 ) ) ;
#15963=ORIENTED_EDGE ( 'NONE', *, *, #12347, .T. ) ;
#15996=LINE ( 'NONE', #21233, #18996 ) ;
#16007=ORIENTED_EDGE ( 'NONE', *, *, #2436, .T. ) ;
#16015=EDGE_CURVE ( 'NONE', #990, #462, #11734, .T. ) ;
#16017=VECTOR ( 'NONE', #348, 1000.000000000000000 ) ;
#16021=DIRECTION ( 'NONE',  ( -1.000000000000000000, 0.000000000000000000, 0.000000000000000000 ) ) ;
#16026=ORIENTED_EDGE ( 'NONE', *, *, #22195, .F. ) ;
#16029=DIRECTION ( 'NONE',  ( -1.000000000000000000, 0.000000000000000000, 0.000000000000000000 ) ) ;
#16035=FACE_OUTER_BOUND ( 'NONE', #15907, .T. ) ;
#16053=CIRCLE ( 'NONE', #14926, 8.749000000000002331 ) ;
#16056=CARTESIAN_POINT ( 'NONE',  ( -20.00005079999999680, 0.000000000000000000, 0.000000000000000000 ) ) ;
#16063=CARTESIAN_POINT ( 'NONE',  ( 4.999999999999999112, 1.464956435139541879, 10.90201369670499076 ) ) ;
#16064=VECTOR ( 'NONE', #7128, 1000.000000000000000 ) ;
#16066=CARTESIAN_POINT ( 'NONE',  ( -10.00000000000000000, 0.000000000000000000, 0.000000000000000000 ) ) ;
#16068=CARTESIAN_POINT ( 'NONE',  ( 0.000000000000000000, 9.241976615262160522, 2.300561732649595736 ) ) ;
#16071=AXIS2_PLACEMENT_3D ( 'NONE', #21986, #1526, #16161 ) ;
#16072=DIRECTION ( 'NONE',  ( -1.000000000000000000, 0.000000000000000000, 0.000000000000000000 ) ) ;
#16074=CARTESIAN_POINT ( 'NONE',  ( 4.999999999999999112, 9.314797388894893615, 1.239665997526919083 ) ) ;
#16076=DIRECTION ( 'NONE',  ( -1.000000000000000000, -0.000000000000000000, 0.000000000000000000 ) ) ;
#16079=CIRCLE ( 'NONE', #12669, 4.000000000000001776 ) ;
#16083=CARTESIAN_POINT ( 'NONE',  ( 4.999999999999999112, -3.174628368996021521, -8.152713396088794084 ) ) ;
#16084=DIRECTION ( 'NONE',  ( 0.000000000000000000, 1.000000000000000000, 3.469446951953611822E-15 ) ) ;
#16097=CIRCLE ( 'NONE', #6534, 11.00000000000000000 ) ;
#16102=VERTEX_POINT ( 'NONE', #5963 ) ;
#16124=ADVANCED_FACE ( 'NONE', ( #22710 ), #19472, .T. ) ;
#16126=ORIENTED_EDGE ( 'NONE', *, *, #12030, .T. ) ;
#16146=ORIENTED_EDGE ( 'NONE', *, *, #9792, .F. ) ;
#16147=CYLINDRICAL_SURFACE ( 'NONE', #11107, 4.000000000000001776 ) ;
#16151=DIRECTION ( 'NONE',  ( 0.000000000000000000, 0.8090169943749485615, -0.5877852522924714718 ) ) ;
#16158=EDGE_CURVE ( 'NONE', #14838, #1746, #1517, .T. ) ;
#16161=DIRECTION ( 'NONE',  ( 0.000000000000000000, 0.000000000000000000, 1.000000000000000000 ) ) ;
#16165=ORIENTED_EDGE ( 'NONE', *, *, #11617, .T. ) ;
#16166=LINE ( 'NONE', #23576, #17575 ) ;
#16172=ORIENTED_EDGE ( 'NONE', *, *, #5258, .F. ) ;
#16176=AXIS2_PLACEMENT_3D ( 'NONE', #13179, #16883, #11516 ) ;
#16192=AXIS2_PLACEMENT_3D ( 'NONE', #10147, #10033, #17321 ) ;
#16204=ORIENTED_EDGE ( 'NONE', *, *, #3794, .T. ) ;
#16208=DIRECTION ( 'NONE',  ( 0.000000000000000000, -0.8090169943749403458, -0.5877852522924830181 ) ) ;
#16210=AXIS2_PLACEMENT_3D ( 'NONE', #4620, #15776, #19222 ) ;
#16217=EDGE_CURVE ( 'NONE', #17794, #19948, #19486, .T. ) ;
#16227=EDGE_CURVE ( 'NONE', #23080, #20778, #13023, .T. ) ;
#16229=VERTEX_POINT ( 'NONE', #6441 ) ;
#16247=EDGE_CURVE ( 'NONE', #11624, #16281, #8814, .T. ) ;
#16251=AXIS2_PLACEMENT_3D ( 'NONE', #8939, #19452, #21586 ) ;
#16252=CARTESIAN_POINT ( 'NONE',  ( 0.000000000000000000, -7.360373001730883935, -4.729683950898952105 ) ) ;
#16256=EDGE_CURVE ( 'NONE', #14554, #16229, #2270, .T. ) ;
#16262=ORIENTED_EDGE ( 'NONE', *, *, #3968, .T. ) ;
#16263=DIRECTION ( 'NONE',  ( 0.000000000000000000, 0.000000000000000000, 1.000000000000000000 ) ) ;
#16264=CARTESIAN_POINT ( 'NONE',  ( 4.999999999999999112, 9.314797388894893615, 5.239665997526921082 ) ) ;
#16273=ORIENTED_EDGE ( 'NONE', *, *, #8663, .F. ) ;
#16281=VERTEX_POINT ( 'NONE', #23543 ) ;
#16288=EDGE_CURVE ( 'NONE', #14427, #9363, #4588, .T. ) ;
#16297=ORIENTED_EDGE ( 'NONE', *, *, #9721, .F. ) ;
#16298=DIRECTION ( 'NONE',  ( -1.000000000000000000, 0.000000000000000000, -0.000000000000000000 ) ) ;
#16311=DIRECTION ( 'NONE',  ( 0.000000000000000000, -1.000000000000000000, -1.040834085586083783E-14 ) ) ;
#16321=CARTESIAN_POINT ( 'NONE',  ( 4.999999999999999112, 3.174628368996190719, -8.152713396088728359 ) ) ;
#16322=VERTEX_POINT ( 'NONE', #3427 ) ;
#16333=AXIS2_PLACEMENT_3D ( 'NONE', #5401, #18211, #9137 ) ;
#16338=CARTESIAN_POINT ( 'NONE',  ( 4.999999999999999112, 0.000000000000000000, 0.000000000000000000 ) ) ;
#16345=CARTESIAN_POINT ( 'NONE',  ( -10.00000000000000000, 0.000000000000000000, 0.000000000000000000 ) ) ;
#16346=VERTEX_POINT ( 'NONE', #16252 ) ;
#16348=SURFACE_SIDE_STYLE ('',( #1832 ) ) ;
#16356=DIRECTION ( 'NONE',  ( -1.000000000000000000, 0.000000000000000000, -0.000000000000000000 ) ) ;
#16358=DIRECTION ( 'NONE',  ( 0.000000000000000000, 0.000000000000000000, -1.000000000000000000 ) ) ;
#16371=CIRCLE ( 'NONE', #4497, 8.749000000000002331 ) ;
#16373=VERTEX_POINT ( 'NONE', #23307 ) ;
#16381=DIRECTION ( 'NONE',  ( -1.000000000000000000, -0.000000000000000000, -0.000000000000000000 ) ) ;
#16386=ORIENTED_EDGE ( 'NONE', *, *, #22195, .T. ) ;
#16413=EDGE_CURVE ( 'NONE', #17247, #16102, #12644, .T. ) ;
#16414=ORIENTED_EDGE ( 'NONE', *, *, #14406, .T. ) ;
#16416=VERTEX_POINT ( 'NONE', #12901 ) ;
#16427=CARTESIAN_POINT ( 'NONE',  ( 4.999999999999999112, 3.174628368996077477, 8.152713396088774545 ) ) ;
#16431=CIRCLE ( 'NONE', #730, 4.000000000000001776 ) ;
#16445=ORIENTED_EDGE ( 'NONE', *, *, #12422, .F. ) ;
#16446=CIRCLE ( 'NONE', #12258, 8.749000000000000554 ) ;
#16449=EDGE_CURVE ( 'NONE', #402, #16416, #10349, .T. ) ;
#16459=AXIS2_PLACEMENT_3D ( 'NONE', #1702, #9046, #23507 ) ;
#16462=DIRECTION ( 'NONE',  ( -1.000000000000000000, -0.000000000000000000, 0.000000000000000000 ) ) ;
#16474=FACE_OUTER_BOUND ( 'NONE', #18898, .T. ) ;
#16491=DIRECTION ( 'NONE',  ( 0.000000000000000000, 0.000000000000000000, 1.000000000000000000 ) ) ;
#16494=CARTESIAN_POINT ( 'NONE',  ( 0.000000000000000000, 0.000000000000000000, 0.000000000000000000 ) ) ;
#16498=ORIENTED_EDGE ( 'NONE', *, *, #16552, .F. ) ;
#16505=CARTESIAN_POINT ( 'NONE',  ( 4.999999999999999112, -6.807171995660630692, 6.478011392632865295 ) ) ;
#16524=ADVANCED_FACE ( 'NONE', ( #18620 ), #9306, .T. ) ;
#16541=EDGE_CURVE ( 'NONE', #17904, #19658, #9195, .T. ) ;
#16542=CIRCLE ( 'NONE', #21871, 8.749000000000002331 ) ;
#16552=EDGE_CURVE ( 'NONE', #1359, #8014, #3038, .T. ) ;
#16560=ORIENTED_EDGE ( 'NONE', *, *, #22356, .F. ) ;
#16566=EDGE_CURVE ( 'NONE', #13420, #16346, #16446, .T. ) ;
#16574=DIRECTION ( 'NONE',  ( 1.000000000000000000, 0.000000000000000000, 0.000000000000000000 ) ) ;
#16576=VECTOR ( 'NONE', #17444, 1000.000000000000000 ) ;
#16578=DIRECTION ( 'NONE',  ( 1.000000000000000000, 0.000000000000000000, 0.000000000000000000 ) ) ;
#16581=( NAMED_UNIT ( * ) SI_UNIT ( $, .STERADIAN. ) SOLID_ANGLE_UNIT ( ) );
#16586=CYLINDRICAL_SURFACE ( 'NONE', #2222, 11.00000000000000000 ) ;
#16594=CIRCLE ( 'NONE', #18877, 11.00000000000000000 ) ;
#16603=LINE ( 'NONE', #12567, #3634 ) ;
#16611=CARTESIAN_POINT ( 'NONE',  ( 4.999999999999999112, -10.90201369670497478, -1.464956435139656898 ) ) ;
#16615=LINE ( 'NONE', #18286, #11839 ) ;
#16618=AXIS2_PLACEMENT_3D ( 'NONE', #7314, #2242, #21881 ) ;
#16640=SHAPE_REPRESENTATION ( 'spur gear_iso_ISO - Spur gear 1M 20T 20PA 5FW ---S20B12H25L8.0S1', ( #7318 ), #23252 ) ;
#16642=EDGE_LOOP ( 'NONE', ( #13813, #15659, #18815, #15209 ) ) ;
#16643=DIRECTION ( 'NONE',  ( -1.000000000000000000, 0.000000000000000000, 0.000000000000000000 ) ) ;
#16660=DIRECTION ( 'NONE',  ( 0.000000000000000000, 0.000000000000000000, 1.000000000000000000 ) ) ;
#16674=VERTEX_POINT ( 'NONE', #1002 ) ;
#16676=AXIS2_PLACEMENT_3D ( 'NONE', #23356, #14158, #17738 ) ;
#16678=EDGE_LOOP ( 'NONE', ( #18905, #2667 ) ) ;
#16679=AXIS2_PLACEMENT_3D ( 'NONE', #13146, #20409, #16491 ) ;
#16683=EDGE_CURVE ( 'NONE', #22841, #3346, #6883, .T. ) ;
#16696=ORIENTED_EDGE ( 'NONE', *, *, #5686, .T. ) ;
#16699=ADVANCED_FACE ( 'NONE', ( #18973 ), #15535, .T. ) ;
#16703=CARTESIAN_POINT ( 'NONE',  ( -10.00000000000000000, 0.000000000000000000, 0.000000000000000000 ) ) ;
#16705=CARTESIAN_POINT ( 'NONE',  ( 4.999999999999999112, -9.314797388894900720, 5.239665997526855357 ) ) ;
#16707=CYLINDRICAL_SURFACE ( 'NONE', #18618, 4.000000000000001776 ) ;
#16717=DIRECTION ( 'NONE',  ( 1.000000000000000000, -0.000000000000000000, -0.000000000000000000 ) ) ;
#16720=CARTESIAN_POINT ( 'NONE',  ( 4.999999999999999112, -3.174628368996021521, -8.152713396088794084 ) ) ;
#16723=CARTESIAN_POINT ( 'NONE',  ( 0.000000000000000000, 0.000000000000000000, 0.000000000000000000 ) ) ;
#16733=CIRCLE ( 'NONE', #14855, 4.000000000000001776 ) ;
#16736=ADVANCED_FACE ( 'NONE', ( #23481 ), #884, .T. ) ;
#16739=AXIS2_PLACEMENT_3D ( 'NONE', #16338, #3153, #7247 ) ;
#16747=LINE ( 'NONE', #328, #2068 ) ;
#16751=LINE ( 'NONE', #16992, #15147 ) ;
#16754=LINE ( 'NONE', #21117, #16576 ) ;
#16758=ORIENTED_EDGE ( 'NONE', *, *, #6897, .F. ) ;
#16759=CARTESIAN_POINT ( 'NONE',  ( 0.000000000000000000, 8.475820894092974456, 4.057423117305423155 ) ) ;
#16765=ORIENTED_EDGE ( 'NONE', *, *, #1108, .T. ) ;
#16771=AXIS2_PLACEMENT_3D ( 'NONE', #21844, #4000, #11459 ) ;
#16776=ORIENTED_EDGE ( 'NONE', *, *, #16015, .F. ) ;
#16787=FACE_OUTER_BOUND ( 'NONE', #21953, .T. ) ;
#16795=AXIS2_PLACEMENT_3D ( 'NONE', #19491, #1165, #2841 ) ;
#16798=ORIENTED_EDGE ( 'NONE', *, *, #10206, .T. ) ;
#16833=ORIENTED_EDGE ( 'NONE', *, *, #19880, .F. ) ;
#16836=AXIS2_PLACEMENT_3D ( 'NONE', #7054, #14374, #1644 ) ;
#16840=VECTOR ( 'NONE', #19357, 1000.000000000000000 ) ;
#16844=ADVANCED_FACE ( 'NONE', ( #9369 ), #7344, .T. ) ;
#16859=DIRECTION ( 'NONE',  ( 1.000000000000000000, 0.000000000000000000, 0.000000000000000000 ) ) ;
#16862=DIRECTION ( 'NONE',  ( -1.000000000000000000, -0.000000000000000000, -0.000000000000000000 ) ) ;
#16864=AXIS2_PLACEMENT_3D ( 'NONE', #23361, #16072, #6966 ) ;
#16868=DIRECTION ( 'NONE',  ( 0.000000000000000000, 0.9510565162951523099, 0.3090169943749515591 ) ) ;
#16870=ORIENTED_EDGE ( 'NONE', *, *, #8663, .T. ) ;
#16874=CARTESIAN_POINT ( 'NONE',  ( 0.000000000000000000, 4.762163868918273479, 9.915734732513236338 ) ) ;
#16876=CIRCLE ( 'NONE', #17257, 11.00000000000000000 ) ;
#16883=DIRECTION ( 'NONE',  ( -1.000000000000000000, -0.000000000000000000, -0.000000000000000000 ) ) ;
#16939=ORIENTED_EDGE ( 'NONE', *, *, #7871, .F. ) ;
#16943=DIRECTION ( 'NONE',  ( -1.000000000000000000, 0.000000000000000000, 0.000000000000000000 ) ) ;
#16954=EDGE_CURVE ( 'NONE', #3506, #2340, #11293, .T. ) ;
#16956=CARTESIAN_POINT ( 'NONE',  ( 0.000000000000000000, 0.000000000000000000, 0.000000000000000000 ) ) ;
#16963=EDGE_LOOP ( 'NONE', ( #9082, #13039, #7132, #23433 ) ) ;
#16969=ORIENTED_EDGE ( 'NONE', *, *, #1321, .F. ) ;
#16972=ORIENTED_EDGE ( 'NONE', *, *, #13747, .T. ) ;
#16976=EDGE_CURVE ( 'NONE', #2926, #4629, #10921, .T. ) ;
#16980=ORIENTED_EDGE ( 'NONE', *, *, #9696, .T. ) ;
#16982=ADVANCED_FACE ( 'NONE', ( #3842 ), #13555, .F. ) ;
#16986=EDGE_CURVE ( 'NONE', #4647, #11669, #15012, .T. ) ;
#16991=PLANE ( 'NONE',  #3244 ) ;
#16992=CARTESIAN_POINT ( 'NONE',  ( 2.499999999999999556, 7.958834565716766285, 7.593217523260609170 ) ) ;
#17005=ORIENTED_EDGE ( 'NONE', *, *, #8238, .T. ) ;
#17015=DIRECTION ( 'NONE',  ( -1.000000000000000000, 0.000000000000000000, -0.000000000000000000 ) ) ;
#17016=CARTESIAN_POINT ( 'NONE',  ( 4.999999999999999112, 0.000000000000000000, 0.000000000000000000 ) ) ;
#17020=CIRCLE ( 'NONE', #14348, 4.000000000000002665 ) ;
#17032=PRODUCT_CONTEXT ( 'NONE', #12233, 'mechanical' ) ;
#17034=CARTESIAN_POINT ( 'NONE',  ( 0.000000000000000000, 1.239665997526886665, 9.314797388894895391 ) ) ;
#17052=CARTESIAN_POINT ( 'NONE',  ( 0.000000000000000000, 9.314797388894893615, 5.239665997526921082 ) ) ;
#17055=VERTEX_POINT ( 'NONE', #20709 ) ;
#17071=DIRECTION ( 'NONE',  ( -1.000000000000000000, 0.000000000000000000, -0.000000000000000000 ) ) ;
#17082=ORIENTED_EDGE ( 'NONE', *, *, #15476, .F. ) ;
#17087=ORIENTED_EDGE ( 'NONE', *, *, #15860, .T. ) ;
#17088=FACE_OUTER_BOUND ( 'NONE', #12146, .T. ) ;
#17091=VERTEX_POINT ( 'NONE', #22267 ) ;
#17097=DIRECTION ( 'NONE',  ( -1.000000000000000000, 0.000000000000000000, 0.000000000000000000 ) ) ;
#17103=ADVANCED_FACE ( 'NONE', ( #4197 ), #7807, .T. ) ;
#17114=CARTESIAN_POINT ( 'NONE',  ( 2.499999999999999556, -7.593217523260523016, -7.958834565716849774 ) ) ;
#17116=CARTESIAN_POINT ( 'NONE',  ( 0.000000000000000000, 0.000000000000000000, 0.000000000000000000 ) ) ;
#17117=EDGE_CURVE ( 'NONE', #5926, #4915, #1698, .T. ) ;
#17125=AXIS2_PLACEMENT_3D ( 'NONE', #14070, #21335, #4956 ) ;
#17129=ORIENTED_EDGE ( 'NONE', *, *, #15308, .T. ) ;
#17130=CIRCLE ( 'NONE', #13315, 4.000000000000001776 ) ;
#17132=FACE_OUTER_BOUND ( 'NONE', #9031, .T. ) ;
#17139=ORIENTED_EDGE ( 'NONE', *, *, #4702, .F. ) ;
#17146=AXIS2_PLACEMENT_3D ( 'NONE', #21423, #21897, #10459 ) ;
#17148=VERTEX_POINT ( 'NONE', #19036 ) ;
#17155=AXIS2_PLACEMENT_3D ( 'NONE', #7738, #11694, #5925 ) ;
#17166=DIRECTION ( 'NONE',  ( 1.000000000000000000, 0.000000000000000000, 0.000000000000000000 ) ) ;
#17168=AXIS2_PLACEMENT_3D ( 'NONE', #1521, #21152, #1984 ) ;
#17182=ORIENTED_EDGE ( 'NONE', *, *, #1139, .T. ) ;
#17186=DIRECTION ( 'NONE',  ( -1.000000000000000000, 0.000000000000000000, -0.000000000000000000 ) ) ;
#17223=AXIS2_PLACEMENT_3D ( 'NONE', #13769, #8374, #18785 ) ;
#17233=FACE_OUTER_BOUND ( 'NONE', #10780, .T. ) ;
#17234=CARTESIAN_POINT ( 'NONE',  ( 4.999999999999999112, -1.239665997526951724, 9.314797388894888286 ) ) ;
#17235=ORIENTED_EDGE ( 'NONE', *, *, #6167, .T. ) ;
#17239=CIRCLE ( 'NONE', #15736, 8.749000000000000554 ) ;
#17241=DIRECTION ( 'NONE',  ( 1.000000000000000000, -0.000000000000000000, -0.000000000000000000 ) ) ;
#17246=CARTESIAN_POINT ( 'NONE',  ( 4.999999999999999112, -1.699438267350307008, -9.241976615262174732 ) ) ;
#17247=VERTEX_POINT ( 'NONE', #14265 ) ;
#17250=DIRECTION ( 'NONE',  ( 0.000000000000000000, 0.3090169943749481174, -0.9510565162951533091 ) ) ;
#17253=EDGE_CURVE ( 'NONE', #17055, #13420, #21525, .T. ) ;
#17256=ORIENTED_EDGE ( 'NONE', *, *, #972, .T. ) ;
#17257=AXIS2_PLACEMENT_3D ( 'NONE', #13800, #2746, #10207 ) ;
#17268=DIRECTION ( 'NONE',  ( 1.000000000000000000, 0.000000000000000000, -0.000000000000000000 ) ) ;
#17269=DIRECTION ( 'NONE',  ( 1.000000000000000000, 0.000000000000000000, -0.000000000000000000 ) ) ;
#17270=VERTEX_POINT ( 'NONE', #21279 ) ;
#17277=AXIS2_PLACEMENT_3D ( 'NONE', #3463, #14020, #17957 ) ;
#17282=EDGE_CURVE ( 'NONE', #7710, #11669, #12459, .T. ) ;
#17307=ORIENTED_EDGE ( 'NONE', *, *, #18167, .T. ) ;
#17321=DIRECTION ( 'NONE',  ( 0.000000000000000000, 0.000000000000000000, 1.000000000000000000 ) ) ;
#17322=CIRCLE ( 'NONE', #4297, 4.000000000000001776 ) ;
#17327=ORIENTED_EDGE ( 'NONE', *, *, #15677, .F. ) ;
#17328=CARTESIAN_POINT ( 'NONE',  ( 2.499999999999999556, 10.82112760146739383, -1.975651141462126059 ) ) ;
#17332=EDGE_LOOP ( 'NONE', ( #2898, #10814, #22813, #21777, #18228, #16445 ) ) ;
#17340=AXIS2_PLACEMENT_3D ( 'NONE', #20714, #8285, #8055 ) ;
#17352=CARTESIAN_POINT ( 'NONE',  ( 0.000000000000000000, 8.152713396088806519, -3.174628368995992655 ) ) ;
#17354=AXIS2_PLACEMENT_3D ( 'NONE', #23097, #6709, #12243 ) ;
#17355=LINE ( 'NONE', #17114, #9018 ) ;
#17358=AXIS2_PLACEMENT_3D ( 'NONE', #20207, #22002, #14741 ) ;
#17368=ORIENTED_EDGE ( 'NONE', *, *, #6402, .F. ) ;
#17379=CARTESIAN_POINT ( 'NONE',  ( 0.000000000000000000, -1.239665997526817165, -9.314797388894906049 ) ) ;
#17382=ORIENTED_EDGE ( 'NONE', *, *, #14674, .T. ) ;
#17391=ORIENTED_EDGE ( 'NONE', *, *, #16256, .F. ) ;
#17393=AXIS2_PLACEMENT_3D ( 'NONE', #8192, #15506, #22774 ) ;
#17410=EDGE_CURVE ( 'NONE', #4211, #6665, #20201, .T. ) ;
#17421=AXIS2_PLACEMENT_3D ( 'NONE', #339, #16298, #18428 ) ;
#17439=AXIS2_PLACEMENT_3D ( 'NONE', #2945, #680, #806 ) ;
#17444=DIRECTION ( 'NONE',  ( 0.000000000000000000, -1.000000000000000000, 0.000000000000000000 ) ) ;
#17445=CARTESIAN_POINT ( 'NONE',  ( 4.999999999999999112, -5.538577986808947529, 6.772677083992368452 ) ) ;
#17450=ADVANCED_FACE ( 'NONE', ( #5489 ), #10680, .T. ) ;
#17452=CIRCLE ( 'NONE', #7117, 8.749000000000004107 ) ;
#17453=ORIENTED_EDGE ( 'NONE', *, *, #3784, .T. ) ;
#17454=VECTOR ( 'NONE', #10538, 1000.000000000000000 ) ;
#17468=DIRECTION ( 'NONE',  ( -1.000000000000000000, -0.000000000000000000, 0.000000000000000000 ) ) ;
#17474=ORIENTED_EDGE ( 'NONE', *, *, #972, .F. ) ;
#17485=CARTESIAN_POINT ( 'NONE',  ( 4.999999999999999112, 7.958834565716766285, 7.593217523260607393 ) ) ;
#17501=CARTESIAN_POINT ( 'NONE',  ( 0.000000000000000000, -1.464956435139620927, 10.90201369670498366 ) ) ;
#17502=VERTEX_POINT ( 'NONE', #18654 ) ;
#17503=AXIS2_PLACEMENT_3D ( 'NONE', #7605, #12883, #14928 ) ;
#17512=DIRECTION ( 'NONE',  ( -1.000000000000000000, -0.000000000000000000, 0.000000000000000000 ) ) ;
#17513=AXIS2_PLACEMENT_3D ( 'NONE', #14247, #14361, #21745 ) ;
#17514=DIRECTION ( 'NONE',  ( 0.000000000000000000, -0.9510565162951499785, -0.3090169943749581649 ) ) ;
#17524=FACE_OUTER_BOUND ( 'NONE', #13034, .T. ) ;
#17527=AXIS2_PLACEMENT_3D ( 'NONE', #4118, #6041, #2434 ) ;
#17540=AXIS2_PLACEMENT_3D ( 'NONE', #14167, #5043, #12375 ) ;
#17549=ADVANCED_FACE ( 'NONE', ( #13171 ), #13525, .T. ) ;
#17557=ADVANCED_FACE ( 'NONE', ( #9695 ), #16991, .T. ) ;
#17559=AXIS2_PLACEMENT_3D ( 'NONE', #9964, #707, #2143 ) ;
#17561=DIRECTION ( 'NONE',  ( 0.000000000000000000, 0.000000000000000000, -1.000000000000000000 ) ) ;
#17575=VECTOR ( 'NONE', #5130, 1000.000000000000000 ) ;
#17590=CARTESIAN_POINT ( 'NONE',  ( -20.00005080000000035, 0.000000000000000000, 0.000000000000000000 ) ) ;
#17591=CARTESIAN_POINT ( 'NONE',  ( 25.00005080000000035, 0.000000000000000000, 1.000000000000000000 ) ) ;
#17592=DIRECTION ( 'NONE',  ( -1.000000000000000000, -0.000000000000000000, 0.000000000000000000 ) ) ;
#17594=ORIENTED_EDGE ( 'NONE', *, *, #20475, .F. ) ;
#17595=AXIS2_PLACEMENT_3D ( 'NONE', #20287, #420, #7747 ) ;
#17597=DIRECTION ( 'NONE',  ( -1.000000000000000000, 0.000000000000000000, 0.000000000000000000 ) ) ;
#17598=DIRECTION ( 'NONE',  ( -1.000000000000000000, 0.000000000000000000, 0.000000000000000000 ) ) ;
#17603=AXIS2_PLACEMENT_3D ( 'NONE', #6542, #2694, #21113 ) ;
#17606=DIRECTION ( 'NONE',  ( 0.000000000000000000, 0.5877852522924688072, 0.8090169943749507819 ) ) ;
#17609=CIRCLE ( 'NONE', #17976, 4.000000000000002665 ) ;
#17612=FACE_OUTER_BOUND ( 'NONE', #8879, .T. ) ;
#17617=DIRECTION ( 'NONE',  ( -1.000000000000000000, 0.000000000000000000, 0.000000000000000000 ) ) ;
#17620=CARTESIAN_POINT ( 'NONE',  ( 4.999999999999999112, 1.239665997527020558, -9.314797388894877628 ) ) ;
#17627=ORIENTED_EDGE ( 'NONE', *, *, #12783, .T. ) ;
#17633=VERTEX_POINT ( 'NONE', #19001 ) ;
#17637=CIRCLE ( 'NONE', #2687, 8.749000000000002331 ) ;
#17638=DIRECTION ( 'NONE',  ( -1.000000000000000000, -0.000000000000000000, 0.000000000000000000 ) ) ;
#17664=FACE_OUTER_BOUND ( 'NONE', #8312, .T. ) ;
#17668=DIRECTION ( 'NONE',  ( -1.000000000000000000, 0.000000000000000000, 0.000000000000000000 ) ) ;
#17683=DIRECTION ( 'NONE',  ( 0.000000000000000000, 0.3090169943749482284, -0.9510565162951534202 ) ) ;
#17684=DIRECTION ( 'NONE',  ( 0.000000000000000000, 0.000000000000000000, -1.000000000000000000 ) ) ;
#17690=LINE ( 'NONE', #21246, #1803 ) ;
#17694=CARTESIAN_POINT ( 'NONE',  ( 4.999999999999999112, -4.472189673936844301, 8.264486777890091673 ) ) ;
#17706=EDGE_CURVE ( 'NONE', #17992, #4647, #5558, .T. ) ;
#17709=ADVANCED_FACE ( 'NONE', ( #17233 ), #6327, .T. ) ;
#17710=DIRECTION ( 'NONE',  ( 0.000000000000000000, 0.000000000000000000, 1.000000000000000000 ) ) ;
#17721=ORIENTED_EDGE ( 'NONE', *, *, #2903, .T. ) ;
#17738=DIRECTION ( 'NONE',  ( 0.000000000000000000, -0.3090169943749349057, -0.9510565162951575280 ) ) ;
#17742=ORIENTED_EDGE ( 'NONE', *, *, #20672, .F. ) ;
#17764=ORIENTED_EDGE ( 'NONE', *, *, #19288, .F. ) ;
#17769=EDGE_CURVE ( 'NONE', #14518, #14298, #6340, .T. ) ;
#17777=FACE_OUTER_BOUND ( 'NONE', #9825, .T. ) ;
#17778=LINE ( 'NONE', #1230, #14845 ) ;
#17786=CARTESIAN_POINT ( 'NONE',  ( 4.999999999999999112, -6.807171995660539210, -6.478011392632959442 ) ) ;
#17789=AXIS2_PLACEMENT_3D ( 'NONE', #15510, #20627, #4235 ) ;
#17793=ORIENTED_EDGE ( 'NONE', *, *, #21984, .F. ) ;
#17794=VERTEX_POINT ( 'NONE', #19240 ) ;
#17816=ADVANCED_FACE ( 'NONE', ( #6445, #15685 ), #1260, .T. ) ;
#17823=CYLINDRICAL_SURFACE ( 'NONE', #16795, 8.749000000000002331 ) ;
#17824=VERTEX_POINT ( 'NONE', #6566 ) ;
#17827=DIRECTION ( 'NONE',  ( 0.000000000000000000, 0.000000000000000000, 1.000000000000000000 ) ) ;
#17838=LINE ( 'NONE', #6706, #2716 ) ;
#17840=CYLINDRICAL_SURFACE ( 'NONE', #17354, 11.00000000000000000 ) ;
#17843=DIRECTION ( 'NONE',  ( 1.000000000000000000, 0.000000000000000000, 0.000000000000000000 ) ) ;
#17844=EDGE_CURVE ( 'NONE', #299, #2926, #18559, .T. ) ;
#17866=CARTESIAN_POINT ( 'NONE',  ( 0.000000000000000000, -9.680994141368808314, 5.222868219166821646 ) ) ;
#17883=ORIENTED_EDGE ( 'NONE', *, *, #1436, .F. ) ;
#17890=LINE ( 'NONE', #14317, #20644 ) ;
#17900=EDGE_CURVE ( 'NONE', #4288, #21750, #16603, .T. ) ;
#17904=VERTEX_POINT ( 'NONE', #23665 ) ;
#17911=DIRECTION ( 'NONE',  ( -1.000000000000000000, -0.000000000000000000, -0.000000000000000000 ) ) ;
#17914=AXIS2_PLACEMENT_3D ( 'NONE', #1339, #4601, #4950 ) ;
#17931=CARTESIAN_POINT ( 'NONE',  ( 0.000000000000000000, -5.538577986808947529, 6.772677083992368452 ) ) ;
#17932=DIRECTION ( 'NONE',  ( -1.000000000000000000, 0.000000000000000000, 0.000000000000000000 ) ) ;
#17936=AXIS2_PLACEMENT_3D ( 'NONE', #7693, #22263, #7804 ) ;
#17957=DIRECTION ( 'NONE',  ( 0.000000000000000000, 0.000000000000000000, 1.000000000000000000 ) ) ;
#17965=DIRECTION ( 'NONE',  ( 0.000000000000000000, 0.000000000000000000, -1.000000000000000000 ) ) ;
#17975=DIRECTION ( 'NONE',  ( 0.000000000000000000, -6.982962677686266711E-15, 1.000000000000000000 ) ) ;
#17976=AXIS2_PLACEMENT_3D ( 'NONE', #20549, #7653, #16868 ) ;
#17983=VECTOR ( 'NONE', #5770, 1000.000000000000000 ) ;
#17992=VERTEX_POINT ( 'NONE', #20168 ) ;
#18001=CYLINDRICAL_SURFACE ( 'NONE', #19400, 4.000000000000002665 ) ;
#18002=EDGE_CURVE ( 'NONE', #22874, #3756, #3433, .T. ) ;
#18005=DIRECTION ( 'NONE',  ( -1.000000000000000000, -0.000000000000000000, -0.000000000000000000 ) ) ;
#18011=EDGE_CURVE ( 'NONE', #23216, #19381, #12480, .T. ) ;
#18031=ORIENTED_EDGE ( 'NONE', *, *, #6885, .T. ) ;
#18037=EDGE_CURVE ( 'NONE', #20184, #18556, #15538, .T. ) ;
#18038=ORIENTED_EDGE ( 'NONE', *, *, #9696, .F. ) ;
#18048=DIRECTION ( 'NONE',  ( -1.000000000000000000, 0.000000000000000000, 0.000000000000000000 ) ) ;
#18056=CARTESIAN_POINT ( 'NONE',  ( 4.999999999999999112, -6.478011392632939014, 6.807171995660559638 ) ) ;
#18059=LINE ( 'NONE', #20304, #1088 ) ;
#18062=EDGE_CURVE ( 'NONE', #19580, #2340, #7632, .T. ) ;
#18067=ORIENTED_EDGE ( 'NONE', *, *, #14702, .T. ) ;
#18072=CARTESIAN_POINT ( 'NONE',  ( 4.999999999999999112, 0.000000000000000000, 0.000000000000000000 ) ) ;
#18074=CARTESIAN_POINT ( 'NONE',  ( 4.999999999999999112, 8.152713396088763886, 3.174628368996105010 ) ) ;
#18079=CIRCLE ( 'NONE', #14969, 11.00000000000000000 ) ;
#18080=EDGE_LOOP ( 'NONE', ( #15881, #10015, #8494, #21210 ) ) ;
#18083=FACE_OUTER_BOUND ( 'NONE', #20487, .T. ) ;
#18102=DIRECTION ( 'NONE',  ( -1.000000000000000000, 0.000000000000000000, 0.000000000000000000 ) ) ;
#18107=VERTEX_POINT ( 'NONE', #18977 ) ;
#18114=EDGE_LOOP ( 'NONE', ( #522, #2400, #15371, #14309 ) ) ;
#18116=CIRCLE ( 'NONE', #19251, 4.000000000000001776 ) ;
#18133=LINE ( 'NONE', #19803, #6305 ) ;
#18134=ORIENTED_EDGE ( 'NONE', *, *, #18167, .F. ) ;
#18137=EDGE_CURVE ( 'NONE', #12645, #9405, #16751, .T. ) ;
#18141=VERTEX_POINT ( 'NONE', #20560 ) ;
#18145=CARTESIAN_POINT ( 'NONE',  ( 0.000000000000000000, 4.729683950898872169, 7.360373001730934561 ) ) ;
#18146=CARTESIAN_POINT ( 'NONE',  ( 4.999999999999999112, 7.593217523260583413, 7.958834565716794707 ) ) ;
#18150=CARTESIAN_POINT ( 'NONE',  ( 4.999999999999999112, 0.000000000000000000, 0.000000000000000000 ) ) ;
#18165=EDGE_CURVE ( 'NONE', #23216, #14554, #1338, .T. ) ;
#18166=ORIENTED_EDGE ( 'NONE', *, *, #2344, .T. ) ;
#18167=EDGE_CURVE ( 'NONE', #5335, #13481, #20844, .T. ) ;
#18169=CYLINDRICAL_SURFACE ( 'NONE', #14841, 8.749000000000002331 ) ;
#18200=CARTESIAN_POINT ( 'NONE',  ( 0.000000000000000000, 0.000000000000000000, 0.000000000000000000 ) ) ;
#18211=DIRECTION ( 'NONE',  ( 1.000000000000000000, 0.000000000000000000, 0.000000000000000000 ) ) ;
#18227=VERTEX_POINT ( 'NONE', #22959 ) ;
#18228=ORIENTED_EDGE ( 'NONE', *, *, #21550, .F. ) ;
#18259=ADVANCED_FACE ( 'NONE', ( #21255 ), #21141, .T. ) ;
#18261=CIRCLE ( 'NONE', #1040, 11.00000000000000000 ) ;
#18264=CARTESIAN_POINT ( 'NONE',  ( 4.999999999999999112, 2.223716399045689407, -8.461683424509292450 ) ) ;
#18271=DIRECTION ( 'NONE',  ( -1.000000000000000000, -0.000000000000000000, 0.000000000000000000 ) ) ;
#18276=ORIENTED_EDGE ( 'NONE', *, *, #16541, .T. ) ;
#18286=CARTESIAN_POINT ( 'NONE',  ( 5.000000000000000000, 0.000000000000000000, 1.000000000000000000 ) ) ;
#18296=EDGE_CURVE ( 'NONE', #12128, #6311, #3648, .T. ) ;
#18299=ADVANCED_FACE ( 'NONE', ( #8138 ), #19479, .T. ) ;
#18300=AXIS2_PLACEMENT_3D ( 'NONE', #16494, #23672, #12802 ) ;
#18309=LINE ( 'NONE', #1539, #5873 ) ;
#18312=AXIS2_PLACEMENT_3D ( 'NONE', #13115, #7721, #9393 ) ;
#18313=ORIENTED_EDGE ( 'NONE', *, *, #22666, .F. ) ;
#18329=EDGE_CURVE ( 'NONE', #16373, #3506, #7506, .T. ) ;
#18346=EDGE_LOOP ( 'NONE', ( #9411, #19046, #21978, #20686 ) ) ;
#18358=EDGE_CURVE ( 'NONE', #3528, #20275, #4378, .T. ) ;
#18397=LINE ( 'NONE', #20294, #20194 ) ;
#18407=DIRECTION ( 'NONE',  ( 0.000000000000000000, 0.000000000000000000, 1.000000000000000000 ) ) ;
#18428=DIRECTION ( 'NONE',  ( 0.000000000000000000, 0.000000000000000000, 1.000000000000000000 ) ) ;
#18433=ORIENTED_EDGE ( 'NONE', *, *, #216, .F. ) ;
#18439=CARTESIAN_POINT ( 'NONE',  ( 4.999999999999999112, 0.000000000000000000, 0.000000000000000000 ) ) ;
#18444=EDGE_CURVE ( 'NONE', #1719, #1746, #6795, .T. ) ;
#18445=AXIS2_PLACEMENT_3D ( 'NONE', #19712, #12445, #15691 ) ;
#18450=CARTESIAN_POINT ( 'NONE',  ( 4.999999999999999112, 9.915734732513218574, 4.762163868918307230 ) ) ;
#18453=ADVANCED_FACE ( 'NONE', ( #21857 ), #19947, .T. ) ;
#18463=EDGE_CURVE ( 'NONE', #13481, #17633, #15164, .T. ) ;
#18495=DIRECTION ( 'NONE',  ( -1.000000000000000000, 0.000000000000000000, -0.000000000000000000 ) ) ;
#18504=CARTESIAN_POINT ( 'NONE',  ( 0.000000000000000000, 0.000000000000000000, 8.749000000000002331 ) ) ;
#18520=EDGE_CURVE ( 'NONE', #20740, #9225, #4427, .T. ) ;
#18529=DIRECTION ( 'NONE',  ( -1.000000000000000000, 0.000000000000000000, 0.000000000000000000 ) ) ;
#18530=CARTESIAN_POINT ( 'NONE',  ( 4.999999999999999112, -8.475820894093002877, 4.057423117305363647 ) ) ;
#18532=DIRECTION ( 'NONE',  ( -1.000000000000000000, 0.000000000000000000, 0.000000000000000000 ) ) ;
#18541=DIRECTION ( 'NONE',  ( 0.000000000000000000, 1.000000000000000000, 3.491481338843133355E-15 ) ) ;
#18542=VECTOR ( 'NONE', #17241, 1000.000000000000000 ) ;
#18548=CARTESIAN_POINT ( 'NONE',  ( 0.000000000000000000, 8.461683424509315543, 2.223716399045600145 ) ) ;
#18556=VERTEX_POINT ( 'NONE', #1973 ) ;
#18557=AXIS2_PLACEMENT_3D ( 'NONE', #5675, #11212, #13129 ) ;
#18559=CIRCLE ( 'NONE', #949, 8.749000000000002331 ) ;
#18564=DIRECTION ( 'NONE',  ( 0.000000000000000000, 0.000000000000000000, 1.000000000000000000 ) ) ;
#18570=AXIS2_PLACEMENT_3D ( 'NONE', #2603, #4410, #13427 ) ;
#18581=AXIS2_PLACEMENT_3D ( 'NONE', #16066, #13925, #6833 ) ;
#18600=ORIENTED_EDGE ( 'NONE', *, *, #551, .T. ) ;
#18601=CARTESIAN_POINT ( 'NONE',  ( 25.00005080000000035, 5.400000000000000355, 1.000000000000000000 ) ) ;
#18613=CYLINDRICAL_SURFACE ( 'NONE', #12553, 4.000000000000001776 ) ;
#18614=EDGE_CURVE ( 'NONE', #22160, #21976, #13391, .T. ) ;
#18618=AXIS2_PLACEMENT_3D ( 'NONE', #14940, #13602, #15174 ) ;
#18620=FACE_OUTER_BOUND ( 'NONE', #18839, .T. ) ;
#18630=CARTESIAN_POINT ( 'NONE',  ( -20.00005079999999680, 0.000000000000000000, 0.000000000000000000 ) ) ;
#18639=LINE ( 'NONE', #6196, #20218 ) ;
#18649=AXIS2_PLACEMENT_3D ( 'NONE', #9773, #17071, #6288 ) ;
#18654=CARTESIAN_POINT ( 'NONE',  ( 0.000000000000000000, 1.464956435139695978, -10.90201369670497122 ) ) ;
#18657=DIRECTION ( 'NONE',  ( -1.000000000000000000, 0.000000000000000000, 0.000000000000000000 ) ) ;
#18669=VERTEX_POINT ( 'NONE', #18504 ) ;
#18675=DIRECTION ( 'NONE',  ( -1.000000000000000000, 0.000000000000000000, 0.000000000000000000 ) ) ;
#18677=VECTOR ( 'NONE', #11811, 1000.000000000000000 ) ;
#18679=STYLED_ITEM ( 'NONE', ( #3288 ), #20459 ) ;
#18692=CYLINDRICAL_SURFACE ( 'NONE', #2678, 4.000000000000001776 ) ;
#18694=ADVANCED_FACE ( 'NONE', ( #13033 ), #20291, .T. ) ;
#18706=VECTOR ( 'NONE', #8743, 1000.000000000000000 ) ;
#18707=ADVANCED_FACE ( 'NONE', ( #7634 ), #14957, .T. ) ;
#18722=AXIS2_PLACEMENT_3D ( 'NONE', #11590, #5812, #7626 ) ;
#18723=ORIENTED_EDGE ( 'NONE', *, *, #871, .F. ) ;
#18726=ORIENTED_EDGE ( 'NONE', *, *, #13309, .F. ) ;
#18734=CARTESIAN_POINT ( 'NONE',  ( 0.000000000000000000, -4.762163868918205978, -9.915734732513268312 ) ) ;
#18749=DIRECTION ( 'NONE',  ( -1.000000000000000000, 0.000000000000000000, 0.000000000000000000 ) ) ;
#18764=CARTESIAN_POINT ( 'NONE',  ( 4.999999999999999112, 4.729683950898977862, -7.360373001730867060 ) ) ;
#18765=VERTEX_POINT ( 'NONE', #10151 ) ;
#18768=AXIS2_PLACEMENT_3D ( 'NONE', #22491, #14876, #5751 ) ;
#18769=ADVANCED_FACE ( 'NONE', ( #18865 ), #2564, .T. ) ;
#18771=AXIS2_PLACEMENT_3D ( 'NONE', #19042, #18928, #4787 ) ;
#18785=DIRECTION ( 'NONE',  ( 0.000000000000000000, 0.000000000000000000, 1.000000000000000000 ) ) ;
#18788=DIRECTION ( 'NONE',  ( -1.000000000000000000, 0.000000000000000000, 0.000000000000000000 ) ) ;
#18790=CYLINDRICAL_SURFACE ( 'NONE', #5555, 8.749000000000002331 ) ;
#18793=EDGE_CURVE ( 'NONE', #7048, #5335, #8472, .T. ) ;
#18794=DIRECTION ( 'NONE',  ( 0.000000000000000000, 0.000000000000000000, 1.000000000000000000 ) ) ;
#18815=ORIENTED_EDGE ( 'NONE', *, *, #16227, .T. ) ;
#18817=ORIENTED_EDGE ( 'NONE', *, *, #11564, .T. ) ;
#18829=EDGE_CURVE ( 'NONE', #17633, #19580, #20424, .T. ) ;
#18839=EDGE_LOOP ( 'NONE', ( #10440, #20, #18600, #16007 ) ) ;
#18865=FACE_OUTER_BOUND ( 'NONE', #9742, .T. ) ;
#18866=ORIENTED_EDGE ( 'NONE', *, *, #8771, .F. ) ;
#18867=CARTESIAN_POINT ( 'NONE',  ( 4.999999999999999112, -4.729683950898921907, 7.360373001730902587 ) ) ;
#18871=ORIENTED_EDGE ( 'NONE', *, *, #7795, .T. ) ;
#18872=DIRECTION ( 'NONE',  ( -1.000000000000000000, 0.000000000000000000, 0.000000000000000000 ) ) ;
#18877=AXIS2_PLACEMENT_3D ( 'NONE', #18150, #9305, #5811 ) ;
#18888=EDGE_CURVE ( 'NONE', #10460, #6517, #23117, .T. ) ;
#18893=ORIENTED_EDGE ( 'NONE', *, *, #19317, .T. ) ;
#18898=EDGE_LOOP ( 'NONE', ( #13781, #6250, #9092, #15963 ) ) ;
#18902=CYLINDRICAL_SURFACE ( 'NONE', #5253, 4.000000000000001776 ) ;
#18905=ORIENTED_EDGE ( 'NONE', *, *, #3074, .T. ) ;
#18908=CARTESIAN_POINT ( 'NONE',  ( 4.999999999999999112, 0.000000000000000000, 0.000000000000000000 ) ) ;
#18910=DIRECTION ( 'NONE',  ( -1.000000000000000000, -0.000000000000000000, -0.000000000000000000 ) ) ;
#18914=CYLINDRICAL_SURFACE ( 'NONE', #21346, 4.000000000000001776 ) ;
#18915=EDGE_CURVE ( 'NONE', #21207, #2537, #18133, .T. ) ;
#18918=VECTOR ( 'NONE', #10885, 1000.000000000000000 ) ;
#18922=CARTESIAN_POINT ( 'NONE',  ( 4.999999999999999112, 8.461683424509345741, -2.223716399045483350 ) ) ;
#18926=AXIS2_PLACEMENT_3D ( 'NONE', #19994, #11051, #22021 ) ;
#18928=DIRECTION ( 'NONE',  ( -1.000000000000000000, 0.000000000000000000, 0.000000000000000000 ) ) ;
#18937=ORIENTED_EDGE ( 'NONE', *, *, #2005, .T. ) ;
#18938=ORIENTED_EDGE ( 'NONE', *, *, #16683, .T. ) ;
#18963=ADVANCED_FACE ( 'NONE', ( #3405, #1711 ), #15883, .F. ) ;
#18973=FACE_OUTER_BOUND ( 'NONE', #7234, .T. ) ;
#18977=CARTESIAN_POINT ( 'NONE',  ( -20.00005080000000035, 7.347880794884120722E-16, 6.000000000000000888 ) ) ;
#18984=ORIENTED_EDGE ( 'NONE', *, *, #21156, .F. ) ;
#18988=EDGE_CURVE ( 'NONE', #12095, #18227, #12069, .T. ) ;
#18996=VECTOR ( 'NONE', #13972, 1000.000000000000000 ) ;
#19001=CARTESIAN_POINT ( 'NONE',  ( 0.000000000000000000, -5.222868219166923787, 9.680994141368751471 ) ) ;
#19002=DIRECTION ( 'NONE',  ( -1.000000000000000000, 0.000000000000000000, 0.000000000000000000 ) ) ;
#19008=CIRCLE ( 'NONE', #8708, 11.00000000000000000 ) ;
#19011=ADVANCED_FACE ( 'NONE', ( #19566 ), #23517, .T. ) ;
#19014=EDGE_CURVE ( 'NONE', #3575, #17091, #21234, .T. ) ;
#19021=EDGE_CURVE ( 'NONE', #8937, #16346, #6892, .T. ) ;
#19023=EDGE_CURVE ( 'NONE', #22160, #19814, #4769, .T. ) ;
#19031=AXIS2_PLACEMENT_3D ( 'NONE', #6522, #2899, #21097 ) ;
#19036=CARTESIAN_POINT ( 'NONE',  ( 0.000000000000000000, 1.975651141462237970, 10.82112760146736896 ) ) ;
#19040=CARTESIAN_POINT ( 'NONE',  ( 4.999999999999999112, 6.807171995660585395, 6.478011392632914145 ) ) ;
#19042=CARTESIAN_POINT ( 'NONE',  ( 4.999999999999999112, 1.699438267350372067, 9.241976615262164074 ) ) ;
#19045=CARTESIAN_POINT ( 'NONE',  ( 0.000000000000000000, 3.174628368996076588, 8.152713396088772768 ) ) ;
#19046=ORIENTED_EDGE ( 'NONE', *, *, #18463, .F. ) ;
#19059=EDGE_CURVE ( 'NONE', #9354, #20516, #17020, .T. ) ;
#19062=CIRCLE ( 'NONE', #9144, 4.000000000000001776 ) ;
#19064=CYLINDRICAL_SURFACE ( 'NONE', #2293, 11.00000000000000000 ) ;
#19083=CARTESIAN_POINT ( 'NONE',  ( 4.999999999999999112, 2.223716399045570835, 8.461683424509324425 ) ) ;
#19091=CIRCLE ( 'NONE', #9172, 11.00000000000000000 ) ;
#19092=DIRECTION ( 'NONE',  ( -1.000000000000000000, -0.000000000000000000, 0.000000000000000000 ) ) ;
#19095=CARTESIAN_POINT ( 'NONE',  ( 4.999999999999999112, 0.000000000000000000, 0.000000000000000000 ) ) ;
#19121=VECTOR ( 'NONE', #20411, 1000.000000000000000 ) ;
#19148=DIRECTION ( 'NONE',  ( -1.000000000000000000, -0.000000000000000000, 0.000000000000000000 ) ) ;
#19150=ORIENTED_EDGE ( 'NONE', *, *, #2874, .T. ) ;
#19160=ORIENTED_EDGE ( 'NONE', *, *, #4130, .F. ) ;
#19163=LINE ( 'NONE', #20940, #8944 ) ;
#19167=ORIENTED_EDGE ( 'NONE', *, *, #21984, .T. ) ;
#19174=EDGE_LOOP ( 'NONE', ( #17627, #22856, #3136, #4110 ) ) ;
#19188=DIRECTION ( 'NONE',  ( -1.000000000000000000, 0.000000000000000000, 0.000000000000000000 ) ) ;
#19194=DIRECTION ( 'NONE',  ( -1.000000000000000000, -0.000000000000000000, 0.000000000000000000 ) ) ;
#19199=EDGE_LOOP ( 'NONE', ( #21153, #1607, #11904, #17721 ) ) ;
#19217=AXIS2_PLACEMENT_3D ( 'NONE', #11262, #213, #7543 ) ;
#19221=ADVANCED_FACE ( 'NONE', ( #8308 ), #862, .T. ) ;
#19222=DIRECTION ( 'NONE',  ( 0.000000000000000000, 0.8090169943749487835, -0.5877852522924714718 ) ) ;
#19240=CARTESIAN_POINT ( 'NONE',  ( 4.999999999999999112, -9.915734732513184824, -4.762163868918378284 ) ) ;
#19244=DIRECTION ( 'NONE',  ( -1.000000000000000000, -0.000000000000000000, -0.000000000000000000 ) ) ;
#19251=AXIS2_PLACEMENT_3D ( 'NONE', #7431, #11028, #21774 ) ;
#19255=ORIENTED_EDGE ( 'NONE', *, *, #18037, .F. ) ;
#19268=CARTESIAN_POINT ( 'NONE',  ( 4.999999999999999112, -1.464956435139466828, -10.90201369670500320 ) ) ;
#19278=ORIENTED_EDGE ( 'NONE', *, *, #3597, .T. ) ;
#19288=EDGE_CURVE ( 'NONE', #15638, #22615, #8197, .T. ) ;
#19290=AXIS2_PLACEMENT_3D ( 'NONE', #5879, #13203, #2392 ) ;
#19298=CARTESIAN_POINT ( 'NONE',  ( 4.999999999999999112, 2.223716399045689407, -8.461683424509292450 ) ) ;
#19317=EDGE_CURVE ( 'NONE', #1746, #22551, #553, .T. ) ;
#19323=CIRCLE ( 'NONE', #11726, 4.000000000000002665 ) ;
#19326=AXIS2_PLACEMENT_3D ( 'NONE', #17234, #6208, #4641 ) ;
#19328=CYLINDRICAL_SURFACE ( 'NONE', #16192, 11.00000000000000000 ) ;
#19332=CARTESIAN_POINT ( 'NONE',  ( 4.999999999999999112, -7.360373001730951437, 4.729683950898845524 ) ) ;
#19333=DIRECTION ( 'NONE',  ( 0.000000000000000000, 0.000000000000000000, 1.000000000000000000 ) ) ;
#19338=CIRCLE ( 'NONE', #14397, 11.00000000000000000 ) ;
#19342=ORIENTED_EDGE ( 'NONE', *, *, #14972, .T. ) ;
#19348=CYLINDRICAL_SURFACE ( 'NONE', #13545, 4.000000000000001776 ) ;
#19349=DIRECTION ( 'NONE',  ( -1.000000000000000000, -0.000000000000000000, 0.000000000000000000 ) ) ;
#19357=DIRECTION ( 'NONE',  ( -1.000000000000000000, -0.000000000000000000, 0.000000000000000000 ) ) ;
#19380=DIRECTION ( 'NONE',  ( -1.000000000000000000, 0.000000000000000000, 0.000000000000000000 ) ) ;
#19381=VERTEX_POINT ( 'NONE', #3135 ) ;
#19387=ORIENTED_EDGE ( 'NONE', *, *, #1108, .F. ) ;
#19390=AXIS2_PLACEMENT_3D ( 'NONE', #14079, #5191, #1349 ) ;
#19400=AXIS2_PLACEMENT_3D ( 'NONE', #22126, #14304, #7548 ) ;
#19409=CARTESIAN_POINT ( 'NONE',  ( 4.999999999999999112, 0.000000000000000000, 0.000000000000000000 ) ) ;
#19410=DIRECTION ( 'NONE',  ( 0.000000000000000000, -0.8090169943749532244, 0.5877852522924653655 ) ) ;
#19413=AXIS2_PLACEMENT_3D ( 'NONE', #5449, #9190, #14583 ) ;
#19421=CARTESIAN_POINT ( 'NONE',  ( 0.000000000000000000, -6.478011392632841314, -6.807171995660652897 ) ) ;
#19424=AXIS2_PLACEMENT_3D ( 'NONE', #3737, #5662, #11201 ) ;
#19426=CARTESIAN_POINT ( 'NONE',  ( 0.000000000000000000, -9.314797388894882957, -1.239665997526988139 ) ) ;
#19438=DIRECTION ( 'NONE',  ( 0.000000000000000000, -0.3090169943749548342, 0.9510565162951509777 ) ) ;
#19451=LINE ( 'NONE', #7130, #6006 ) ;
#19452=DIRECTION ( 'NONE',  ( -1.000000000000000000, 0.000000000000000000, 0.000000000000000000 ) ) ;
#19463=CARTESIAN_POINT ( 'NONE',  ( 4.999999999999999112, 7.360373001730986964, -4.729683950898791345 ) ) ;
#19472=CYLINDRICAL_SURFACE ( 'NONE', #11495, 4.000000000000001776 ) ;
#19479=CYLINDRICAL_SURFACE ( 'NONE', #14726, 4.000000000000001776 ) ;
#19482=CARTESIAN_POINT ( 'NONE',  ( 4.999999999999999112, -9.241976615262146311, -1.699438267350473097 ) ) ;
#19485=VERTEX_POINT ( 'NONE', #19045 ) ;
#19486=CIRCLE ( 'NONE', #3811, 4.000000000000001776 ) ;
#19491=CARTESIAN_POINT ( 'NONE',  ( 4.999999999999999112, 0.000000000000000000, 0.000000000000000000 ) ) ;
#19504=FACE_OUTER_BOUND ( 'NONE', #6219, .T. ) ;
#19508=DIRECTION ( 'NONE',  ( 1.000000000000000000, -0.000000000000000000, -0.000000000000000000 ) ) ;
#19510=ORIENTED_EDGE ( 'NONE', *, *, #13206, .F. ) ;
#19528=CARTESIAN_POINT ( 'NONE',  ( 0.000000000000000000, 0.000000000000000000, 0.000000000000000000 ) ) ;
#19545=CARTESIAN_POINT ( 'NONE',  ( 4.999999999999999112, 0.000000000000000000, 0.000000000000000000 ) ) ;
#19565=LINE ( 'NONE', #3522, #9470 ) ;
#19566=FACE_OUTER_BOUND ( 'NONE', #8476, .T. ) ;
#19573=DIRECTION ( 'NONE',  ( -1.000000000000000000, 0.000000000000000000, -0.000000000000000000 ) ) ;
#19580=VERTEX_POINT ( 'NONE', #5033 ) ;
#19583=CIRCLE ( 'NONE', #18445, 4.000000000000001776 ) ;
#19598=DIRECTION ( 'NONE',  ( 0.000000000000000000, -0.3090169943749551673, 0.9510565162951511997 ) ) ;
#19603=EDGE_LOOP ( 'NONE', ( #2569, #19342, #16126, #21969 ) ) ;
#19613=CARTESIAN_POINT ( 'NONE',  ( 4.999999999999999112, -9.680994141368810091, 5.222868219166821646 ) ) ;
#19614=DIRECTION ( 'NONE',  ( -1.000000000000000000, 0.000000000000000000, 0.000000000000000000 ) ) ;
#19619=EDGE_LOOP ( 'NONE', ( #11391, #19510, #6342, #10966 ) ) ;
#19653=ORIENTED_EDGE ( 'NONE', *, *, #10631, .F. ) ;
#19658=VERTEX_POINT ( 'NONE', #17501 ) ;
#19661=ORIENTED_EDGE ( 'NONE', *, *, #7795, .F. ) ;
#19689=DIRECTION ( 'NONE',  ( -1.000000000000000000, -0.000000000000000000, -0.000000000000000000 ) ) ;
#19695=DIRECTION ( 'NONE',  ( -1.000000000000000000, 0.000000000000000000, 0.000000000000000000 ) ) ;
#19700=DIRECTION ( 'NONE',  ( 0.000000000000000000, 0.000000000000000000, 1.000000000000000000 ) ) ;
#19708=ORIENTED_EDGE ( 'NONE', *, *, #14204, .F. ) ;
#19709=DIRECTION ( 'NONE',  ( 1.000000000000000000, -0.000000000000000000, -0.000000000000000000 ) ) ;
#19710=EDGE_CURVE ( 'NONE', #872, #3547, #15521, .T. ) ;
#19712=CARTESIAN_POINT ( 'NONE',  ( 4.999999999999999112, 6.807171995660585395, 6.478011392632914145 ) ) ;
#19714=FACE_OUTER_BOUND ( 'NONE', #12016, .T. ) ;
#19715=CARTESIAN_POINT ( 'NONE',  ( 4.999999999999999112, 0.000000000000000000, 0.000000000000000000 ) ) ;
#19732=ADVANCED_FACE ( 'NONE', ( #9462 ), #20211, .T. ) ;
#19738=CARTESIAN_POINT ( 'NONE',  ( 4.999999999999999112, 1.975651141462391402, -10.82112760146734054 ) ) ;
#19763=CIRCLE ( 'NONE', #17503, 4.000000000000001776 ) ;
#19770=VERTEX_POINT ( 'NONE', #7199 ) ;
#19779=VERTEX_POINT ( 'NONE', #11092 ) ;
#19780=AXIS2_PLACEMENT_3D ( 'NONE', #3195, #10541, #14482 ) ;
#19789=CIRCLE ( 'NONE', #22851, 4.000000000000001776 ) ;
#19793=CARTESIAN_POINT ( 'NONE',  ( 25.00005080000000035, 0.000000000000000000, 0.000000000000000000 ) ) ;
#19796=CIRCLE ( 'NONE', #19031, 4.000000000000000000 ) ;
#19803=CARTESIAN_POINT ( 'NONE',  ( 2.499999999999999556, 10.82112760146736363, 1.975651141462276161 ) ) ;
#19814=VERTEX_POINT ( 'NONE', #1897 ) ;
#19829=CARTESIAN_POINT ( 'NONE',  ( 4.999999999999999112, 7.360373001730920350, 4.729683950898897926 ) ) ;
#19830=AXIS2_PLACEMENT_3D ( 'NONE', #17246, #817, #22730 ) ;
#19836=ORIENTED_EDGE ( 'NONE', *, *, #22823, .F. ) ;
#19846=CYLINDRICAL_SURFACE ( 'NONE', #21766, 4.000000000000000888 ) ;
#19847=CIRCLE ( 'NONE', #9556, 11.00000000000000000 ) ;
#19857=CARTESIAN_POINT ( 'NONE',  ( 4.999999999999999112, 3.174628368996077477, 8.152713396088774545 ) ) ;
#19859=AXIS2_PLACEMENT_3D ( 'NONE', #1147, #12323, #2712 ) ;
#19861=ORIENTED_EDGE ( 'NONE', *, *, #22256, .F. ) ;
#19880=EDGE_CURVE ( 'NONE', #3988, #1063, #17355, .T. ) ;
#19882=VECTOR ( 'NONE', #11741, 1000.000000000000000 ) ;
#19905=DIRECTION ( 'NONE',  ( 0.000000000000000000, 0.000000000000000000, 1.000000000000000000 ) ) ;
#19908=EDGE_CURVE ( 'NONE', #2402, #11644, #6092, .T. ) ;
#19923=CARTESIAN_POINT ( 'NONE',  ( 0.000000000000000000, 0.000000000000000000, 0.000000000000000000 ) ) ;
#19924=VERTEX_POINT ( 'NONE', #9593 ) ;
#19931=CARTESIAN_POINT ( 'NONE',  ( 0.000000000000000000, 0.000000000000000000, 0.000000000000000000 ) ) ;
#19935=DIRECTION ( 'NONE',  ( -1.000000000000000000, 0.000000000000000000, 0.000000000000000000 ) ) ;
#19939=DIRECTION ( 'NONE',  ( 0.000000000000000000, -0.5877852522924624790, -0.8090169943749553338 ) ) ;
#19947=CYLINDRICAL_SURFACE ( 'NONE', #2123, 11.00000000000000000 ) ;
#19948=VERTEX_POINT ( 'NONE', #11385 ) ;
#19952=ORIENTED_EDGE ( 'NONE', *, *, #241, .T. ) ;
#19961=DIRECTION ( 'NONE',  ( -1.000000000000000000, -0.000000000000000000, 0.000000000000000000 ) ) ;
#19975=FACE_OUTER_BOUND ( 'NONE', #22243, .T. ) ;
#19994=CARTESIAN_POINT ( 'NONE',  ( 0.000000000000000000, 6.478011392632982535, -6.807171995660517005 ) ) ;
#19999=ORIENTED_EDGE ( 'NONE', *, *, #22684, .F. ) ;
#20006=ADVANCED_FACE ( 'NONE', ( #4173 ), #18790, .T. ) ;
#20025=LINE ( 'NONE', #18601, #7553 ) ;
#20037=ORIENTED_EDGE ( 'NONE', *, *, #4702, .T. ) ;
#20053=ORIENTED_EDGE ( 'NONE', *, *, #16976, .F. ) ;
#20059=EDGE_LOOP ( 'NONE', ( #2431, #23188, #12009, #9376 ) ) ;
#20066=LINE ( 'NONE', #12920, #13746 ) ;
#20094=ORIENTED_EDGE ( 'NONE', *, *, #23090, .T. ) ;
#20097=AXIS2_PLACEMENT_3D ( 'NONE', #19482, #16029, #8720 ) ;
#20102=ORIENTED_EDGE ( 'NONE', *, *, #5551, .T. ) ;
#20104=DIRECTION ( 'NONE',  ( -1.000000000000000000, 0.000000000000000000, 0.000000000000000000 ) ) ;
#20112=FACE_OUTER_BOUND ( 'NONE', #3503, .T. ) ;
#20143=( NAMED_UNIT ( * ) SI_UNIT ( $, .STERADIAN. ) SOLID_ANGLE_UNIT ( ) );
#20150=CYLINDRICAL_SURFACE ( 'NONE', #9131, 4.000000000000001776 ) ;
#20154=CARTESIAN_POINT ( 'NONE',  ( 4.999999999999999112, 6.772677083992387992, 5.538577986808924436 ) ) ;
#20160=EDGE_CURVE ( 'NONE', #19948, #18765, #12545, .T. ) ;
#20161=LINE ( 'NONE', #18264, #13550 ) ;
#20168=CARTESIAN_POINT ( 'NONE',  ( 4.999999999999999112, -6.772677083992425295, 5.538577986808878251 ) ) ;
#20183=DIRECTION ( 'NONE',  ( 0.000000000000000000, 1.000000000000000000, 0.000000000000000000 ) ) ;
#20184=VERTEX_POINT ( 'NONE', #162 ) ;
#20194=VECTOR ( 'NONE', #2094, 1000.000000000000000 ) ;
#20201=LINE ( 'NONE', #22110, #22344 ) ;
#20207=CARTESIAN_POINT ( 'NONE',  ( 4.999999999999999112, -1.699438267350307008, -9.241976615262174732 ) ) ;
#20208=AXIS2_PLACEMENT_3D ( 'NONE', #17016, #13668, #22502 ) ;
#20211=CYLINDRICAL_SURFACE ( 'NONE', #17421, 8.749000000000002331 ) ;
#20218=VECTOR ( 'NONE', #9923, 1000.000000000000000 ) ;
#20236=AXIS2_PLACEMENT_3D ( 'NONE', #8690, #16462, #3157 ) ;
#20240=DIRECTION ( 'NONE',  ( 0.000000000000000000, 0.000000000000000000, 1.000000000000000000 ) ) ;
#20250=AXIS2_PLACEMENT_3D ( 'NONE', #4838, #15653, #1562 ) ;
#20262=CIRCLE ( 'NONE', #16836, 4.000000000000001776 ) ;
#20272=CIRCLE ( 'NONE', #9596, 4.000000000000001776 ) ;
#20274=CARTESIAN_POINT ( 'NONE',  ( 0.000000000000000000, 0.000000000000000000, -6.000000000000000888 ) ) ;
#20275=VERTEX_POINT ( 'NONE', #20274 ) ;
#20277=EDGE_CURVE ( 'NONE', #12317, #9363, #13364, .T. ) ;
#20287=CARTESIAN_POINT ( 'NONE',  ( 0.000000000000000000, -4.472189673936844301, 8.264486777890091673 ) ) ;
#20291=CYLINDRICAL_SURFACE ( 'NONE', #212, 4.000000000000001776 ) ;
#20292=ORIENTED_EDGE ( 'NONE', *, *, #12757, .F. ) ;
#20294=CARTESIAN_POINT ( 'NONE',  ( 2.499999999999999556, -1.464956435139620039, 10.90201369670498366 ) ) ;
#20296=CIRCLE ( 'NONE', #10024, 4.000000000000001776 ) ;
#20304=CARTESIAN_POINT ( 'NONE',  ( 5.000000000000000000, 0.000000000000000000, -1.000000000000000000 ) ) ;
#20305=ORIENTED_EDGE ( 'NONE', *, *, #9792, .T. ) ;
#20311=ORIENTED_EDGE ( 'NONE', *, *, #20757, .F. ) ;
#20322=CARTESIAN_POINT ( 'NONE',  ( 0.000000000000000000, 10.90201369670498721, -1.464956435139581403 ) ) ;
#20327=DIRECTION ( 'NONE',  ( 0.000000000000000000, 0.000000000000000000, 1.000000000000000000 ) ) ;
#20337=CARTESIAN_POINT ( 'NONE',  ( 25.00005080000000035, 0.000000000000000000, 0.000000000000000000 ) ) ;
#20344=DIRECTION ( 'NONE',  ( -1.000000000000000000, -0.000000000000000000, 0.000000000000000000 ) ) ;
#20345=AXIS2_PLACEMENT_3D ( 'NONE', #12745, #18102, #16084 ) ;
#20351=CARTESIAN_POINT ( 'NONE',  ( 4.999999999999999112, 4.057423117305393845, 8.475820894092990443 ) ) ;
#20362=ADVANCED_FACE ( 'NONE', ( #22058 ), #15165, .T. ) ;
#20381=AXIS2_PLACEMENT_3D ( 'NONE', #19095, #17668, #19438 ) ;
#20397=CARTESIAN_POINT ( 'NONE',  ( 4.999999999999999112, -1.239665997526951724, 9.314797388894888286 ) ) ;
#20409=DIRECTION ( 'NONE',  ( -1.000000000000000000, -0.000000000000000000, -0.000000000000000000 ) ) ;
#20411=DIRECTION ( 'NONE',  ( 1.000000000000000000, -0.000000000000000000, -0.000000000000000000 ) ) ;
#20412=FACE_OUTER_BOUND ( 'NONE', #716, .T. ) ;
#20414=ORIENTED_EDGE ( 'NONE', *, *, #6310, .T. ) ;
#20424=CIRCLE ( 'NONE', #12834, 11.00000000000000000 ) ;
#20432=CARTESIAN_POINT ( 'NONE',  ( 4.999999999999999112, 8.734705317681626724, -0.4999240074894757413 ) ) ;
#20433=EDGE_CURVE ( 'NONE', #5230, #22394, #4032, .T. ) ;
#20438=DIRECTION ( 'NONE',  ( -1.000000000000000000, -0.000000000000000000, 0.000000000000000000 ) ) ;
#20450=VECTOR ( 'NONE', #18048, 1000.000000000000000 ) ;
#20454=ORIENTED_EDGE ( 'NONE', *, *, #7671, .F. ) ;
#20459=ADVANCED_BREP_SHAPE_REPRESENTATION ( '', ( #14725, #7318 ), #23252 ) ;
#20463=AXIS2_PLACEMENT_3D ( 'NONE', #732, #13336, #11780 ) ;
#20475=EDGE_CURVE ( 'NONE', #18765, #15228, #19323, .T. ) ;
#20478=CIRCLE ( 'NONE', #13626, 11.00000000000000000 ) ;
#20487=EDGE_LOOP ( 'NONE', ( #12555, #6158, #3079, #19387 ) ) ;
#20489=ORIENTED_EDGE ( 'NONE', *, *, #16158, .F. ) ;
#20512=ORIENTED_EDGE ( 'NONE', *, *, #6174, .T. ) ;
#20515=FACE_OUTER_BOUND ( 'NONE', #14224, .T. ) ;
#20516=VERTEX_POINT ( 'NONE', #15025 ) ;
#20530=AXIS2_PLACEMENT_3D ( 'NONE', #7087, #16076, #16311 ) ;
#20533=LINE ( 'NONE', #17328, #12281 ) ;
#20543=DIRECTION ( 'NONE',  ( 0.000000000000000000, 0.000000000000000000, 1.000000000000000000 ) ) ;
#20545=AXIS2_PLACEMENT_3D ( 'NONE', #4025, #16859, #9319 ) ;
#20549=CARTESIAN_POINT ( 'NONE',  ( 0.000000000000000000, 1.699438267350372067, 9.241976615262164074 ) ) ;
#20560=CARTESIAN_POINT ( 'NONE',  ( 0.000000000000000000, -1.464956435139469049, -10.90201369670500497 ) ) ;
#20565=EDGE_LOOP ( 'NONE', ( #17368, #9836, #23643, #16939 ) ) ;
#20596=DIRECTION ( 'NONE',  ( -1.000000000000000000, 0.000000000000000000, -0.000000000000000000 ) ) ;
#20599=VERTEX_POINT ( 'NONE', #11065 ) ;
#20602=ORIENTED_EDGE ( 'NONE', *, *, #17769, .T. ) ;
#20604=EDGE_LOOP ( 'NONE', ( #791, #12985, #11185, #20037 ) ) ;
#20616=AXIS2_PLACEMENT_3D ( 'NONE', #8752, #23100, #3222 ) ;
#20626=ORIENTED_EDGE ( 'NONE', *, *, #6501, .F. ) ;
#20627=DIRECTION ( 'NONE',  ( -1.000000000000000000, -0.000000000000000000, 0.000000000000000000 ) ) ;
#20636=CARTESIAN_POINT ( 'NONE',  ( 4.999999999999999112, 8.152713396088806519, -3.174628368995992655 ) ) ;
#20644=VECTOR ( 'NONE', #1467, 1000.000000000000000 ) ;
#20664=EDGE_LOOP ( 'NONE', ( #20937, #11432, #3262, #544 ) ) ;
#20668=CYLINDRICAL_SURFACE ( 'NONE', #21373, 11.00000000000000000 ) ;
#20669=AXIS2_PLACEMENT_3D ( 'NONE', #20337, #18675, #15113 ) ;
#20672=EDGE_CURVE ( 'NONE', #21998, #15638, #23538, .T. ) ;
#20686=ORIENTED_EDGE ( 'NONE', *, *, #18329, .T. ) ;
#20687=PLANE ( 'NONE',  #6736 ) ;
#20692=CARTESIAN_POINT ( 'NONE',  ( 0.000000000000000000, 0.000000000000000000, 0.000000000000000000 ) ) ;
#20693=DIRECTION ( 'NONE',  ( -1.000000000000000000, 0.000000000000000000, 0.000000000000000000 ) ) ;
#20696=ORIENTED_EDGE ( 'NONE', *, *, #3938, .F. ) ;
#20704=DIRECTION ( 'NONE',  ( 0.000000000000000000, 0.000000000000000000, 1.000000000000000000 ) ) ;
#20709=CARTESIAN_POINT ( 'NONE',  ( 4.999999999999999112, -6.772677083992345359, -5.538577986808975062 ) ) ;
#20711=FACE_OUTER_BOUND ( 'NONE', #3580, .T. ) ;
#20714=CARTESIAN_POINT ( 'NONE',  ( 0.000000000000000000, 0.000000000000000000, 0.000000000000000000 ) ) ;
#20718=ORIENTED_EDGE ( 'NONE', *, *, #7871, .T. ) ;
#20722=VERTEX_POINT ( 'NONE', #4327 ) ;
#20725=ORIENTED_EDGE ( 'NONE', *, *, #6331, .T. ) ;
#20737=CARTESIAN_POINT ( 'NONE',  ( 0.000000000000000000, -5.222868219166784343, -9.680994141368829631 ) ) ;
#20740=VERTEX_POINT ( 'NONE', #957 ) ;
#20750=LINE ( 'NONE', #20636, #12960 ) ;
#20757=EDGE_CURVE ( 'NONE', #4629, #2957, #15161, .T. ) ;
#20762=CARTESIAN_POINT ( 'NONE',  ( 4.999999999999999112, 0.000000000000000000, 0.000000000000000000 ) ) ;
#20764=AXIS2_PLACEMENT_3D ( 'NONE', #22772, #1087, #13473 ) ;
#20778=VERTEX_POINT ( 'NONE', #610 ) ;
#20781=ORIENTED_EDGE ( 'NONE', *, *, #2932, .T. ) ;
#20794=CARTESIAN_POINT ( 'NONE',  ( 4.999999999999999112, -4.057423117305452465, 8.475820894092962021 ) ) ;
#20798=EDGE_CURVE ( 'NONE', #18765, #7419, #15559, .T. ) ;
#20799=DIRECTION ( 'NONE',  ( 0.000000000000000000, 0.000000000000000000, 1.000000000000000000 ) ) ;
#20800=DIRECTION ( 'NONE',  ( 0.000000000000000000, 0.000000000000000000, 1.000000000000000000 ) ) ;
#20823=CARTESIAN_POINT ( 'NONE',  ( 2.499999999999999556, -7.958834565716820464, 7.593217523260554103 ) ) ;
#20824=AXIS2_PLACEMENT_3D ( 'NONE', #16759, #13070, #22123 ) ;
#20825=DIRECTION ( 'NONE',  ( -1.000000000000000000, -0.000000000000000000, -0.000000000000000000 ) ) ;
#20829=CARTESIAN_POINT ( 'NONE',  ( 4.999999999999999112, -4.762163868918343645, 9.915734732513202587 ) ) ;
#20838=ORIENTED_EDGE ( 'NONE', *, *, #16986, .T. ) ;
#20839=ORIENTED_EDGE ( 'NONE', *, *, #15860, .F. ) ;
#20844=CIRCLE ( 'NONE', #23540, 8.749000000000002331 ) ;
#20853=CARTESIAN_POINT ( 'NONE',  ( 4.999999999999999112, -9.241976615262146311, -1.699438267350473097 ) ) ;
#20872=CARTESIAN_POINT ( 'NONE',  ( 4.999999999999999112, -8.734705317681623171, -0.4999240074895356933 ) ) ;
#20890=ORIENTED_EDGE ( 'NONE', *, *, #10726, .F. ) ;
#20898=ADVANCED_FACE ( 'NONE', ( #10343 ), #1549, .T. ) ;
#20905=VECTOR ( 'NONE', #11400, 1000.000000000000000 ) ;
#20907=ORIENTED_EDGE ( 'NONE', *, *, #13083, .T. ) ;
#20910=CIRCLE ( 'NONE', #20545, 4.000000000000000888 ) ;
#20920=EDGE_CURVE ( 'NONE', #11384, #10460, #3277, .T. ) ;
#20923=CIRCLE ( 'NONE', #6811, 8.749000000000002331 ) ;
#20929=AXIS2_PLACEMENT_3D ( 'NONE', #1519, #8503, #17710 ) ;
#20937=ORIENTED_EDGE ( 'NONE', *, *, #4130, .T. ) ;
#20940=CARTESIAN_POINT ( 'NONE',  ( 25.00005080000000035, 0.000000000000000000, 4.000000000000000000 ) ) ;
#20954=DIRECTION ( 'NONE',  ( -1.000000000000000000, -0.000000000000000000, -0.000000000000000000 ) ) ;
#20962=CARTESIAN_POINT ( 'NONE',  ( 0.000000000000000000, -4.729683950898817102, -7.360373001730970977 ) ) ;
#20965=CARTESIAN_POINT ( 'NONE',  ( 0.000000000000000000, -8.475820894092946034, -4.057423117305485327 ) ) ;
#20976=ORIENTED_EDGE ( 'NONE', *, *, #11701, .T. ) ;
#20982=PRODUCT_DEFINITION_SHAPE ( 'NONE', 'NONE',  #7275 ) ;
#20987=CARTESIAN_POINT ( 'NONE',  ( 0.000000000000000000, -6.772677083992345359, -5.538577986808975062 ) ) ;
#21000=ADVANCED_FACE ( 'NONE', ( #5268 ), #12251, .T. ) ;
#21003=ORIENTED_EDGE ( 'NONE', *, *, #8948, .T. ) ;
#21020=CARTESIAN_POINT ( 'NONE',  ( 4.999999999999999112, -6.478011392632841314, -6.807171995660652897 ) ) ;
#21027=CARTESIAN_POINT ( 'NONE',  ( 0.000000000000000000, 0.000000000000000000, 0.000000000000000000 ) ) ;
#21028=ORIENTED_EDGE ( 'NONE', *, *, #6110, .T. ) ;
#21040=ORIENTED_EDGE ( 'NONE', *, *, #12347, .F. ) ;
#21043=CARTESIAN_POINT ( 'NONE',  ( 0.000000000000000000, 4.729683950898977862, -7.360373001730867060 ) ) ;
#21052=FACE_OUTER_BOUND ( 'NONE', #7192, .T. ) ;
#21061=CYLINDRICAL_SURFACE ( 'NONE', #13914, 11.00000000000000000 ) ;
#21078=DIRECTION ( 'NONE',  ( 0.000000000000000000, 0.000000000000000000, 1.000000000000000000 ) ) ;
#21096=ORIENTED_EDGE ( 'NONE', *, *, #14943, .T. ) ;
#21097=DIRECTION ( 'NONE',  ( 0.000000000000000000, 8.881784197001252323E-16, 1.000000000000000000 ) ) ;
#21100=VERTEX_POINT ( 'NONE', #13075 ) ;
#21113=DIRECTION ( 'NONE',  ( 0.000000000000000000, 0.000000000000000000, 1.000000000000000000 ) ) ;
#21117=CARTESIAN_POINT ( 'NONE',  ( -20.00005080000000035, 0.000000000000000000, 1.000000000000000000 ) ) ;
#21132=EDGE_CURVE ( 'NONE', #14572, #11205, #7437, .T. ) ;
#21140=CARTESIAN_POINT ( 'NONE',  ( -10.00000000000000000, 0.000000000000000000, 0.000000000000000000 ) ) ;
#21141=CYLINDRICAL_SURFACE ( 'NONE', #11674, 8.749000000000002331 ) ;
#21142=ORIENTED_EDGE ( 'NONE', *, *, #6567, .F. ) ;
#21143=FACE_OUTER_BOUND ( 'NONE', #19603, .T. ) ;
#21145=DIRECTION ( 'NONE',  ( 0.000000000000000000, 0.000000000000000000, 1.000000000000000000 ) ) ;
#21152=DIRECTION ( 'NONE',  ( -1.000000000000000000, 0.000000000000000000, 0.000000000000000000 ) ) ;
#21153=ORIENTED_EDGE ( 'NONE', *, *, #13905, .F. ) ;
#21156=EDGE_CURVE ( 'NONE', #15687, #7993, #8008, .T. ) ;
#21174=ORIENTED_EDGE ( 'NONE', *, *, #21466, .T. ) ;
#21198=DIRECTION ( 'NONE',  ( 0.000000000000000000, 0.000000000000000000, 1.000000000000000000 ) ) ;
#21207=VERTEX_POINT ( 'NONE', #9709 ) ;
#21210=ORIENTED_EDGE ( 'NONE', *, *, #2932, .F. ) ;
#21217=CARTESIAN_POINT ( 'NONE',  ( 4.999999999999999112, 9.314797388894909602, -1.239665997526783858 ) ) ;
#21233=CARTESIAN_POINT ( 'NONE',  ( 4.999999999999999112, 0.4999240074894452657, 8.734705317681628500 ) ) ;
#21234=LINE ( 'NONE', #5322, #3614 ) ;
#21246=CARTESIAN_POINT ( 'NONE',  ( 4.999999999999999112, 6.772677083992387992, 5.538577986808924436 ) ) ;
#21255=FACE_OUTER_BOUND ( 'NONE', #4179, .T. ) ;
#21263=CARTESIAN_POINT ( 'NONE',  ( 0.000000000000000000, 0.000000000000000000, 0.000000000000000000 ) ) ;
#21275=DIRECTION ( 'NONE',  ( 0.000000000000000000, 0.000000000000000000, 1.000000000000000000 ) ) ;
#21276=DIRECTION ( 'NONE',  ( -1.000000000000000000, -0.000000000000000000, -0.000000000000000000 ) ) ;
#21279=CARTESIAN_POINT ( 'NONE',  ( 4.999999999999999112, -2.223716399045630343, 8.461683424509308438 ) ) ;
#21280=AXIS2_PLACEMENT_3D ( 'NONE', #20397, #19935, #5808 ) ;
#21281=DIRECTION ( 'NONE',  ( -1.000000000000000000, 0.000000000000000000, 0.000000000000000000 ) ) ;
#21310=CYLINDRICAL_SURFACE ( 'NONE', #10341, 4.000000000000001776 ) ;
#21323=EDGE_CURVE ( 'NONE', #22906, #11604, #13373, .T. ) ;
#21326=CARTESIAN_POINT ( 'NONE',  ( 4.999999999999999112, -5.538577986808947529, 6.772677083992368452 ) ) ;
#21327=VECTOR ( 'NONE', #3621, 1000.000000000000000 ) ;
#21328=ORIENTED_EDGE ( 'NONE', *, *, #9721, .T. ) ;
#21335=DIRECTION ( 'NONE',  ( -1.000000000000000000, -0.000000000000000000, -0.000000000000000000 ) ) ;
#21336=VECTOR ( 'NONE', #10184, 1000.000000000000000 ) ;
#21340=DIRECTION ( 'NONE',  ( 0.000000000000000000, 0.000000000000000000, 1.000000000000000000 ) ) ;
#21341=CARTESIAN_POINT ( 'NONE',  ( 0.000000000000000000, 0.000000000000000000, 0.000000000000000000 ) ) ;
#21343=EDGE_CURVE ( 'NONE', #11403, #21998, #1275, .T. ) ;
#21346=AXIS2_PLACEMENT_3D ( 'NONE', #6355, #2741, #6473 ) ;
#21350=DIRECTION ( 'NONE',  ( 1.000000000000000000, 0.000000000000000000, 0.000000000000000000 ) ) ;
#21356=ORIENTED_EDGE ( 'NONE', *, *, #20672, .T. ) ;
#21364=VECTOR ( 'NONE', #10798, 1000.000000000000000 ) ;
#21373=AXIS2_PLACEMENT_3D ( 'NONE', #9797, #16862, #20543 ) ;
#21386=AXIS2_PLACEMENT_3D ( 'NONE', #15062, #18749, #14821 ) ;
#21395=ADVANCED_FACE ( 'NONE', ( #21631 ), #17823, .T. ) ;
#21402=ORIENTED_EDGE ( 'NONE', *, *, #8370, .T. ) ;
#21423=CARTESIAN_POINT ( 'NONE',  ( 0.000000000000000000, 0.000000000000000000, 0.000000000000000000 ) ) ;
#21439=CIRCLE ( 'NONE', #10406, 4.000000000000001776 ) ;
#21448=ORIENTED_EDGE ( 'NONE', *, *, #18165, .F. ) ;
#21455=CYLINDRICAL_SURFACE ( 'NONE', #17125, 11.00000000000000000 ) ;
#21466=EDGE_CURVE ( 'NONE', #4915, #18669, #3319, .T. ) ;
#21469=CARTESIAN_POINT ( 'NONE',  ( 5.000000000000000888, 0.000000000000000000, 0.000000000000000000 ) ) ;
#21470=DIRECTION ( 'NONE',  ( -1.000000000000000000, 0.000000000000000000, 0.000000000000000000 ) ) ;
#21473=SURFACE_STYLE_USAGE ( .BOTH. , #16348 ) ;
#21483=EDGE_CURVE ( 'NONE', #22874, #17270, #21740, .T. ) ;
#21487=EDGE_CURVE ( 'NONE', #18107, #3528, #20066, .T. ) ;
#21493=EDGE_CURVE ( 'NONE', #11604, #10342, #12983, .T. ) ;
#21502=CARTESIAN_POINT ( 'NONE',  ( 2.499999999999999556, -1.975651141462163363, -10.82112760146738673 ) ) ;
#21503=CARTESIAN_POINT ( 'NONE',  ( 2.499999999999999556, -10.90201369670499965, 1.464956435139506352 ) ) ;
#21507=DIRECTION ( 'NONE',  ( 0.000000000000000000, 0.000000000000000000, 1.000000000000000000 ) ) ;
#21514=CARTESIAN_POINT ( 'NONE',  ( 0.000000000000000000, 1.975651141462390514, -10.82112760146734232 ) ) ;
#21515=DIRECTION ( 'NONE',  ( 0.000000000000000000, 0.000000000000000000, 1.000000000000000000 ) ) ;
#21525=LINE ( 'NONE', #10446, #4002 ) ;
#21529=ORIENTED_EDGE ( 'NONE', *, *, #14204, .T. ) ;
#21550=EDGE_CURVE ( 'NONE', #12867, #11644, #16615, .T. ) ;
#21554=CARTESIAN_POINT ( 'NONE',  ( 4.999999999999999112, -7.958834565716820464, 7.593217523260553214 ) ) ;
#21557=ORIENTED_EDGE ( 'NONE', *, *, #12783, .F. ) ;
#21568=ORIENTED_EDGE ( 'NONE', *, *, #8240, .T. ) ;
#21572=VECTOR ( 'NONE', #22507, 1000.000000000000000 ) ;
#21577=CYLINDRICAL_SURFACE ( 'NONE', #502, 4.000000000000000000 ) ;
#21584=ORIENTED_EDGE ( 'NONE', *, *, #4567, .T. ) ;
#21586=DIRECTION ( 'NONE',  ( 0.000000000000000000, -6.938893903907226800E-15, 1.000000000000000000 ) ) ;
#21594=ORIENTED_EDGE ( 'NONE', *, *, #18358, .F. ) ;
#21604=EDGE_CURVE ( 'NONE', #15248, #15525, #18059, .T. ) ;
#21605=CARTESIAN_POINT ( 'NONE',  ( 2.499999999999999556, 7.593217523260583413, 7.958834565716794707 ) ) ;
#21608=AXIS2_PLACEMENT_3D ( 'NONE', #2943, #4517, #1032 ) ;
#21616=AXIS2_PLACEMENT_3D ( 'NONE', #17116, #15219, #15458 ) ;
#21625=CYLINDRICAL_SURFACE ( 'NONE', #17513, 4.000000000000001776 ) ;
#21631=FACE_OUTER_BOUND ( 'NONE', #15428, .T. ) ;
#21637=CARTESIAN_POINT ( 'NONE',  ( 4.999999999999999112, -8.264486777890139635, 4.472189673936757259 ) ) ;
#21660=DIRECTION ( 'NONE',  ( -1.000000000000000000, 0.000000000000000000, -0.000000000000000000 ) ) ;
#21691=ORIENTED_EDGE ( 'NONE', *, *, #18137, .F. ) ;
#21710=DIRECTION ( 'NONE',  ( 0.000000000000000000, 0.000000000000000000, -1.000000000000000000 ) ) ;
#21722=AXIS2_PLACEMENT_3D ( 'NONE', #19426, #1105, #13718 ) ;
#21740=CIRCLE ( 'NONE', #17168, 8.749000000000002331 ) ;
#21742=CARTESIAN_POINT ( 'NONE',  ( -20.00005080000000035, 5.400000000000000355, 0.000000000000000000 ) ) ;
#21745=DIRECTION ( 'NONE',  ( 0.000000000000000000, 0.000000000000000000, 1.000000000000000000 ) ) ;
#21750=VERTEX_POINT ( 'NONE', #7874 ) ;
#21761=EDGE_CURVE ( 'NONE', #12101, #20275, #15081, .T. ) ;
#21766=AXIS2_PLACEMENT_3D ( 'NONE', #21637, #19961, #5241 ) ;
#21774=DIRECTION ( 'NONE',  ( 0.000000000000000000, 0.8090169943749445647, 0.5877852522924772449 ) ) ;
#21777=ORIENTED_EDGE ( 'NONE', *, *, #7093, .F. ) ;
#21783=CARTESIAN_POINT ( 'NONE',  ( 2.499999999999999556, 4.762163868918273479, 9.915734732513236338 ) ) ;
#21789=CIRCLE ( 'NONE', #16459, 4.000000000000001776 ) ;
#21792=EDGE_CURVE ( 'NONE', #23080, #1931, #18639, .T. ) ;
#21793=( NAMED_UNIT ( * ) SI_UNIT ( $, .STERADIAN. ) SOLID_ANGLE_UNIT ( ) );
#21800=CARTESIAN_POINT ( 'NONE',  ( 4.999999999999999112, 0.000000000000000000, 0.000000000000000000 ) ) ;
#21804=DIRECTION ( 'NONE',  ( 0.000000000000000000, -6.938893903907225222E-15, 1.000000000000000000 ) ) ;
#21807=ADVANCED_FACE ( 'NONE', ( #15195 ), #20668, .T. ) ;
#21819=ORIENTED_EDGE ( 'NONE', *, *, #7889, .T. ) ;
#21844=CARTESIAN_POINT ( 'NONE',  ( 4.999999999999999112, 0.000000000000000000, 0.000000000000000000 ) ) ;
#21848=CARTESIAN_POINT ( 'NONE',  ( 4.999999999999999112, 0.000000000000000000, 0.000000000000000000 ) ) ;
#21855=CARTESIAN_POINT ( 'NONE',  ( 4.999999999999999112, 0.000000000000000000, 0.000000000000000000 ) ) ;
#21857=FACE_OUTER_BOUND ( 'NONE', #22129, .T. ) ;
#21864=CARTESIAN_POINT ( 'NONE',  ( 4.999999999999999112, 8.475820894092974456, 4.057423117305423155 ) ) ;
#21871=AXIS2_PLACEMENT_3D ( 'NONE', #13530, #18788, #15453 ) ;
#21881=DIRECTION ( 'NONE',  ( 0.000000000000000000, 0.000000000000000000, 1.000000000000000000 ) ) ;
#21893=ORIENTED_EDGE ( 'NONE', *, *, #2960, .F. ) ;
#21897=DIRECTION ( 'NONE',  ( -1.000000000000000000, -0.000000000000000000, -0.000000000000000000 ) ) ;
#21903=ORIENTED_EDGE ( 'NONE', *, *, #2709, .T. ) ;
#21920=EDGE_LOOP ( 'NONE', ( #22522, #5036, #7162, #20907 ) ) ;
#21953=EDGE_LOOP ( 'NONE', ( #1101, #19150, #17182, #1021 ) ) ;
#21960=VECTOR ( 'NONE', #4972, 1000.000000000000000 ) ;
#21961=DIRECTION ( 'NONE',  ( 0.000000000000000000, 0.5877852522924742473, -0.8090169943749466741 ) ) ;
#21966=DIRECTION ( 'NONE',  ( 0.000000000000000000, 1.000000000000000000, 3.469446951953611822E-15 ) ) ;
#21969=ORIENTED_EDGE ( 'NONE', *, *, #18011, .T. ) ;
#21970=CARTESIAN_POINT ( 'NONE',  ( 5.000000000000000888, 4.898587196589412829E-16, -4.000000000000000000 ) ) ;
#21971=DIRECTION ( 'NONE',  ( -1.000000000000000000, -0.000000000000000000, -0.000000000000000000 ) ) ;
#21976=VERTEX_POINT ( 'NONE', #1611 ) ;
#21978=ORIENTED_EDGE ( 'NONE', *, *, #12379, .F. ) ;
#21984=EDGE_CURVE ( 'NONE', #17502, #10342, #55, .T. ) ;
#21986=CARTESIAN_POINT ( 'NONE',  ( 4.999999999999999112, 0.000000000000000000, 0.000000000000000000 ) ) ;
#21996=AXIS2_PLACEMENT_3D ( 'NONE', #19545, #14187, #16208 ) ;
#21998=VERTEX_POINT ( 'NONE', #18145 ) ;
#22001=VECTOR ( 'NONE', #12569, 1000.000000000000000 ) ;
#22002=DIRECTION ( 'NONE',  ( -1.000000000000000000, 0.000000000000000000, -0.000000000000000000 ) ) ;
#22008=ORIENTED_EDGE ( 'NONE', *, *, #9929, .T. ) ;
#22017=LINE ( 'NONE', #7564, #3387 ) ;
#22021=DIRECTION ( 'NONE',  ( 0.000000000000000000, -0.3090169943749350168, -0.9510565162951576390 ) ) ;
#22028=ORIENTED_EDGE ( 'NONE', *, *, #18888, .F. ) ;
#22047=EDGE_CURVE ( 'NONE', #12818, #1359, #16431, .T. ) ;
#22058=FACE_OUTER_BOUND ( 'NONE', #13783, .T. ) ;
#22062=FACE_OUTER_BOUND ( 'NONE', #1333, .T. ) ;
#22063=EDGE_LOOP ( 'NONE', ( #19167, #15277, #7551, #9052 ) ) ;
#22082=EDGE_LOOP ( 'NONE', ( #13974, #9944, #1600, #4119 ) ) ;
#22083=DIRECTION ( 'NONE',  ( 1.000000000000000000, 0.000000000000000000, 0.000000000000000000 ) ) ;
#22087=ORIENTED_EDGE ( 'NONE', *, *, #13779, .T. ) ;
#22095=DIRECTION ( 'NONE',  ( -1.000000000000000000, -0.000000000000000000, -0.000000000000000000 ) ) ;
#22105=CYLINDRICAL_SURFACE ( 'NONE', #8796, 4.000000000000001776 ) ;
#22110=CARTESIAN_POINT ( 'NONE',  ( 4.999999999999999112, 0.4999240074895661690, -8.734705317681621395 ) ) ;
#22115=ADVANCED_FACE ( 'NONE', ( #1090 ), #21310, .T. ) ;
#22123=DIRECTION ( 'NONE',  ( 0.000000000000000000, 0.8090169943749485615, -0.5877852522924714718 ) ) ;
#22124=CARTESIAN_POINT ( 'NONE',  ( 4.999999999999999112, 0.000000000000000000, 0.000000000000000000 ) ) ;
#22126=CARTESIAN_POINT ( 'NONE',  ( 4.999999999999999112, 6.478011392632890164, 6.807171995660607600 ) ) ;
#22129=EDGE_LOOP ( 'NONE', ( #16833, #13834, #8830, #16297 ) ) ;
#22134=DIRECTION ( 'NONE',  ( 0.000000000000000000, -0.5877852522924624790, -0.8090169943749551118 ) ) ;
#22135=CIRCLE ( 'NONE', #3783, 4.000000000000001776 ) ;
#22151=LINE ( 'NONE', #22272, #17983 ) ;
#22160=VERTEX_POINT ( 'NONE', #16083 ) ;
#22168=AXIS2_PLACEMENT_3D ( 'NONE', #5289, #239, #2034 ) ;
#22192=ORIENTED_EDGE ( 'NONE', *, *, #6200, .F. ) ;
#22195=EDGE_CURVE ( 'NONE', #8728, #12130, #22537, .T. ) ;
#22197=AXIS2_PLACEMENT_3D ( 'NONE', #12475, #21281, #8878 ) ;
#22208=ORIENTED_EDGE ( 'NONE', *, *, #871, .T. ) ;
#22209=LINE ( 'NONE', #11356, #19121 ) ;
#22210=DIRECTION ( 'NONE',  ( 0.000000000000000000, 0.000000000000000000, 1.000000000000000000 ) ) ;
#22211=CARTESIAN_POINT ( 'NONE',  ( 4.999999999999999112, 8.734705317681626724, 0.4999240074894746311 ) ) ;
#22213=VERTEX_POINT ( 'NONE', #17866 ) ;
#22235=CARTESIAN_POINT ( 'NONE',  ( 4.999999999999999112, 5.538577986808900455, 6.772677083992405755 ) ) ;
#22237=CARTESIAN_POINT ( 'NONE',  ( 0.000000000000000000, 0.000000000000000000, 0.000000000000000000 ) ) ;
#22243=EDGE_LOOP ( 'NONE', ( #18866, #10080, #21557, #3233 ) ) ;
#22245=LINE ( 'NONE', #11156, #4145 ) ;
#22248=ORIENTED_EDGE ( 'NONE', *, *, #15533, .F. ) ;
#22251=CARTESIAN_POINT ( 'NONE',  ( -20.00005080000000035, 0.000000000000000000, -1.000000000000000000 ) ) ;
#22255=CARTESIAN_POINT ( 'NONE',  ( 4.999999999999999112, 7.593217523260696211, -7.958834565716683684 ) ) ;
#22256=EDGE_CURVE ( 'NONE', #22912, #15687, #19847, .T. ) ;
#22259=ORIENTED_EDGE ( 'NONE', *, *, #9725, .F. ) ;
#22260=EDGE_CURVE ( 'NONE', #8348, #23470, #22916, .T. ) ;
#22262=VECTOR ( 'NONE', #17592, 1000.000000000000000 ) ;
#22263=DIRECTION ( 'NONE',  ( -1.000000000000000000, 0.000000000000000000, -0.000000000000000000 ) ) ;
#22264=CIRCLE ( 'NONE', #20345, 4.000000000000002665 ) ;
#22267=CARTESIAN_POINT ( 'NONE',  ( 0.000000000000000000, -9.241976615262146311, 2.300561732649528679 ) ) ;
#22272=CARTESIAN_POINT ( 'NONE',  ( 4.999999999999999112, -0.4999240074895051067, 8.734705317681624948 ) ) ;
#22278=VERTEX_POINT ( 'NONE', #1623 ) ;
#22301=ORIENTED_EDGE ( 'NONE', *, *, #5298, .T. ) ;
#22307=ORIENTED_EDGE ( 'NONE', *, *, #14674, .F. ) ;
#22325=EDGE_CURVE ( 'NONE', #18556, #12818, #15067, .T. ) ;
#22327=ORIENTED_EDGE ( 'NONE', *, *, #8238, .F. ) ;
#22331=ORIENTED_EDGE ( 'NONE', *, *, #21483, .F. ) ;
#22337=CARTESIAN_POINT ( 'NONE',  ( -20.00005080000000035, 0.000000000000000000, -6.000000000000000888 ) ) ;
#22338=VERTEX_POINT ( 'NONE', #295 ) ;
#22344=VECTOR ( 'NONE', #14503, 1000.000000000000000 ) ;
#22350=CARTESIAN_POINT ( 'NONE',  ( 0.000000000000000000, 4.472189673936902921, -8.264486777890061475 ) ) ;
#22356=EDGE_CURVE ( 'NONE', #17055, #8937, #11109, .T. ) ;
#22361=DIRECTION ( 'NONE',  ( -1.000000000000000000, 0.000000000000000000, 0.000000000000000000 ) ) ;
#22385=CARTESIAN_POINT ( 'NONE',  ( 4.999999999999999112, 0.000000000000000000, 0.000000000000000000 ) ) ;
#22394=VERTEX_POINT ( 'NONE', #15306 ) ;
#22411=DIRECTION ( 'NONE',  ( 1.000000000000000000, 0.000000000000000000, 0.000000000000000000 ) ) ;
#22430=EDGE_LOOP ( 'NONE', ( #19999, #14506, #17793, #9592 ) ) ;
#22447=DIRECTION ( 'NONE',  ( 0.000000000000000000, 0.000000000000000000, 1.000000000000000000 ) ) ;
#22451=ORIENTED_EDGE ( 'NONE', *, *, #2367, .F. ) ;
#22456=ORIENTED_EDGE ( 'NONE', *, *, #13903, .F. ) ;
#22491=CARTESIAN_POINT ( 'NONE',  ( 0.000000000000000000, 0.000000000000000000, 0.000000000000000000 ) ) ;
#22494=ORIENTED_EDGE ( 'NONE', *, *, #16247, .T. ) ;
#22496=MECHANICAL_DESIGN_GEOMETRIC_PRESENTATION_REPRESENTATION('',(#18679),#8742);
#22502=DIRECTION ( 'NONE',  ( 0.000000000000000000, 0.5877852522924685852, 0.8090169943749506709 ) ) ;
#22507=DIRECTION ( 'NONE',  ( -1.000000000000000000, 0.000000000000000000, 0.000000000000000000 ) ) ;
#22513=CARTESIAN_POINT ( 'NONE',  ( 2.499999999999999556, -10.90201369670497655, -1.464956435139657343 ) ) ;
#22522=ORIENTED_EDGE ( 'NONE', *, *, #3069, .T. ) ;
#22524=ORIENTED_EDGE ( 'NONE', *, *, #14062, .F. ) ;
#22529=AXIS2_PLACEMENT_3D ( 'NONE', #1179, #3100, #21275 ) ;
#22537=CIRCLE ( 'NONE', #5703, 8.749000000000002331 ) ;
#22538=FACE_OUTER_BOUND ( 'NONE', #3327, .T. ) ;
#22542=ADVANCED_FACE ( 'NONE', ( #12062 ), #2917, .T. ) ;
#22548=AXIS2_PLACEMENT_3D ( 'NONE', #4131, #6051, #7981 ) ;
#22549=EDGE_LOOP ( 'NONE', ( #20838, #12748, #8699, #13539 ) ) ;
#22551=VERTEX_POINT ( 'NONE', #4731 ) ;
#22556=ORIENTED_EDGE ( 'NONE', *, *, #2344, .F. ) ;
#22558=CARTESIAN_POINT ( 'NONE',  ( 4.999999999999999112, 1.699438267350500409, -9.241976615262139205 ) ) ;
#22568=CYLINDRICAL_SURFACE ( 'NONE', #14093, 4.000000000000001776 ) ;
#22570=FACE_OUTER_BOUND ( 'NONE', #16963, .T. ) ;
#22589=CARTESIAN_POINT ( 'NONE',  ( 4.999999999999999112, 1.699438267350372067, 9.241976615262164074 ) ) ;
#22590=CARTESIAN_POINT ( 'NONE',  ( 0.000000000000000000, -6.772677083992425295, 5.538577986808878251 ) ) ;
#22593=VECTOR ( 'NONE', #12496, 1000.000000000000000 ) ;
#22598=ORIENTED_EDGE ( 'NONE', *, *, #18002, .F. ) ;
#22601=CARTESIAN_POINT ( 'NONE',  ( 0.000000000000000000, 8.734705317681626724, -0.4999240074894757413 ) ) ;
#22609=CARTESIAN_POINT ( 'NONE',  ( 4.999999999999999112, -7.593217523260637591, 7.958834565716740528 ) ) ;
#22613=DIRECTION ( 'NONE',  ( 0.000000000000000000, 0.9510565162951545304, -0.3090169943749446757 ) ) ;
#22615=VERTEX_POINT ( 'NONE', #1596 ) ;
#22626=EDGE_LOOP ( 'NONE', ( #14718, #2013, #3175, #3113 ) ) ;
#22637=DIRECTION ( 'NONE',  ( -1.000000000000000000, -0.000000000000000000, -0.000000000000000000 ) ) ;
#22655=CARTESIAN_POINT ( 'NONE',  ( 0.000000000000000000, 9.915734732513218574, 4.762163868918309007 ) ) ;
#22657=CYLINDRICAL_SURFACE ( 'NONE', #10072, 11.00000000000000000 ) ;
#22666=EDGE_CURVE ( 'NONE', #4211, #990, #4975, .T. ) ;
#22668=VERTEX_POINT ( 'NONE', #8936 ) ;
#22677=DIRECTION ( 'NONE',  ( 0.000000000000000000, 0.000000000000000000, 1.000000000000000000 ) ) ;
#22684=EDGE_CURVE ( 'NONE', #11604, #9577, #6888, .T. ) ;
#22696=ORIENTED_EDGE ( 'NONE', *, *, #5457, .F. ) ;
#22705=PRODUCT_DEFINITION_CONTEXT ( 'detailed design', #5946, 'design' ) ;
#22710=FACE_OUTER_BOUND ( 'NONE', #8550, .T. ) ;
#22720=DIRECTION ( 'NONE',  ( -1.000000000000000000, -0.000000000000000000, -0.000000000000000000 ) ) ;
#22730=DIRECTION ( 'NONE',  ( 0.000000000000000000, -0.9510565162951500895, -0.3090169943749582204 ) ) ;
#22745=CARTESIAN_POINT ( 'NONE',  ( 25.00005080000000035, 0.000000000000000000, 0.000000000000000000 ) ) ;
#22751=AXIS2_PLACEMENT_3D ( 'NONE', #22385, #4314, #11767 ) ;
#22760=VERTEX_POINT ( 'NONE', #2182 ) ;
#22762=VERTEX_POINT ( 'NONE', #11570 ) ;
#22772=CARTESIAN_POINT ( 'NONE',  ( 4.999999999999999112, 8.475820894092974456, 4.057423117305423155 ) ) ;
#22774=DIRECTION ( 'NONE',  ( 0.000000000000000000, 0.000000000000000000, 1.000000000000000000 ) ) ;
#22776=CARTESIAN_POINT ( 'NONE',  ( 4.999999999999999112, -3.174628368996134320, 8.152713396088753228 ) ) ;
#22784=AXIS2_PLACEMENT_3D ( 'NONE', #21027, #10178, #15686 ) ;
#22788=LINE ( 'NONE', #19083, #18677 ) ;
#22813=ORIENTED_EDGE ( 'NONE', *, *, #1145, .F. ) ;
#22823=EDGE_CURVE ( 'NONE', #3756, #19580, #7302, .T. ) ;
#22826=DIRECTION ( 'NONE',  ( 0.000000000000000000, -0.8090169943749530024, 0.5877852522924653655 ) ) ;
#22835=ORIENTED_EDGE ( 'NONE', *, *, #1306, .T. ) ;
#22841=VERTEX_POINT ( 'NONE', #17052 ) ;
#22851=AXIS2_PLACEMENT_3D ( 'NONE', #15588, #19148, #22854 ) ;
#22854=DIRECTION ( 'NONE',  ( 0.000000000000000000, -0.9510565162951500895, -0.3090169943749582204 ) ) ;
#22856=ORIENTED_EDGE ( 'NONE', *, *, #19317, .F. ) ;
#22859=CARTESIAN_POINT ( 'NONE',  ( 2.499999999999999556, -9.680994141368733708, -5.222868219166961978 ) ) ;
#22863=CARTESIAN_POINT ( 'NONE',  ( 0.000000000000000000, -4.057423117305452465, 8.475820894092962021 ) ) ;
#22865=DIRECTION ( 'NONE',  ( 1.000000000000000000, -0.000000000000000000, -0.000000000000000000 ) ) ;
#22869=LINE ( 'NONE', #9729, #15064 ) ;
#22872=COLOUR_RGB ( '', 0.72549020, 0.75294118, 0.79215686) ;
#22874=VERTEX_POINT ( 'NONE', #22776 ) ;
#22880=CIRCLE ( 'NONE', #1444, 11.00000000000000000 ) ;
#22883=ORIENTED_EDGE ( 'NONE', *, *, #12915, .T. ) ;
#22890=DIRECTION ( 'NONE',  ( -1.000000000000000000, 0.000000000000000000, 0.000000000000000000 ) ) ;
#22892=CARTESIAN_POINT ( 'NONE',  ( 4.999999999999999112, 0.4999240074894452657, 8.734705317681628500 ) ) ;
#22906=VERTEX_POINT ( 'NONE', #19298 ) ;
#22912=VERTEX_POINT ( 'NONE', #3009 ) ;
#22914=CARTESIAN_POINT ( 'NONE',  ( 4.999999999999999112, -9.314797388894900720, 1.239665997526853580 ) ) ;
#22916=CIRCLE ( 'NONE', #12628, 4.000000000000002665 ) ;
#22922=FACE_OUTER_BOUND ( 'NONE', #15259, .T. ) ;
#22924=AXIS2_PLACEMENT_3D ( 'NONE', #3541, #9198, #19700 ) ;
#22932=DIRECTION ( 'NONE',  ( -1.000000000000000000, 0.000000000000000000, 0.000000000000000000 ) ) ;
#22943=CARTESIAN_POINT ( 'NONE',  ( 4.999999999999999112, 0.000000000000000000, 0.000000000000000000 ) ) ;
#22946=CIRCLE ( 'NONE', #6070, 4.000000000000001776 ) ;
#22949=EDGE_CURVE ( 'NONE', #2643, #3575, #16079, .T. ) ;
#22954=DIRECTION ( 'NONE',  ( 0.000000000000000000, 0.3090169943749481174, -0.9510565162951533091 ) ) ;
#22959=CARTESIAN_POINT ( 'NONE',  ( 0.000000000000000000, -10.90201369670499965, 1.464956435139506352 ) ) ;
#22971=CYLINDRICAL_SURFACE ( 'NONE', #6801, 4.000000000000001776 ) ;
#22982=ORIENTED_EDGE ( 'NONE', *, *, #6055, .F. ) ;
#22989=DIRECTION ( 'NONE',  ( 0.000000000000000000, 1.000000000000000000, 3.469446951953612611E-15 ) ) ;
#22993=DIRECTION ( 'NONE',  ( -1.000000000000000000, 0.000000000000000000, 0.000000000000000000 ) ) ;
#23055=DIRECTION ( 'NONE',  ( 0.000000000000000000, 0.000000000000000000, -1.000000000000000000 ) ) ;
#23059=CIRCLE ( 'NONE', #12395, 4.000000000000001776 ) ;
#23073=DIRECTION ( 'NONE',  ( -1.000000000000000000, -0.000000000000000000, 0.000000000000000000 ) ) ;
#23074=EDGE_CURVE ( 'NONE', #10244, #1974, #20272, .T. ) ;
#23076=AXIS2_PLACEMENT_3D ( 'NONE', #2799, #15178, #6291 ) ;
#23080=VERTEX_POINT ( 'NONE', #2663 ) ;
#23090=EDGE_CURVE ( 'NONE', #22668, #2142, #13832, .T. ) ;
#23095=CARTESIAN_POINT ( 'NONE',  ( 5.000000000000000888, 3.872983346207417021, 1.000000000000000000 ) ) ;
#23097=CARTESIAN_POINT ( 'NONE',  ( -10.00000000000000000, 0.000000000000000000, 0.000000000000000000 ) ) ;
#23100=DIRECTION ( 'NONE',  ( -1.000000000000000000, -0.000000000000000000, -0.000000000000000000 ) ) ;
#23102=ORIENTED_EDGE ( 'NONE', *, *, #7889, .F. ) ;
#23117=CIRCLE ( 'NONE', #5537, 4.000000000000001776 ) ;
#23140=VECTOR ( 'NONE', #537, 1000.000000000000000 ) ;
#23142=ORIENTED_EDGE ( 'NONE', *, *, #1306, .F. ) ;
#23149=DIRECTION ( 'NONE',  ( 0.000000000000000000, 0.000000000000000000, 1.000000000000000000 ) ) ;
#23166=EDGE_LOOP ( 'NONE', ( #11087, #14604, #4827, #18166 ) ) ;
#23170=ORIENTED_EDGE ( 'NONE', *, *, #16247, .F. ) ;
#23177=FACE_OUTER_BOUND ( 'NONE', #20565, .T. ) ;
#23182=DIRECTION ( 'NONE',  ( 0.000000000000000000, 0.000000000000000000, 1.000000000000000000 ) ) ;
#23188=ORIENTED_EDGE ( 'NONE', *, *, #19014, .T. ) ;
#23200=DIRECTION ( 'NONE',  ( 1.000000000000000000, 0.000000000000000000, -0.000000000000000000 ) ) ;
#23203=CARTESIAN_POINT ( 'NONE',  ( 0.000000000000000000, 2.223716399045689407, -8.461683424509292450 ) ) ;
#23209=VECTOR ( 'NONE', #15867, 1000.000000000000000 ) ;
#23210=DIRECTION ( 'NONE',  ( -1.000000000000000000, -0.000000000000000000, -0.000000000000000000 ) ) ;
#23216=VERTEX_POINT ( 'NONE', #8782 ) ;
#23229=DIRECTION ( 'NONE',  ( -1.000000000000000000, 0.000000000000000000, -0.000000000000000000 ) ) ;
#23246=AXIS2_PLACEMENT_3D ( 'NONE', #15756, #13714, #14190 ) ;
#23252=( GEOMETRIC_REPRESENTATION_CONTEXT ( 3 ) GLOBAL_UNCERTAINTY_ASSIGNED_CONTEXT ( ( #2580 ) ) GLOBAL_UNIT_ASSIGNED_CONTEXT ( ( #9292, #12417, #16581 ) ) REPRESENTATION_CONTEXT ( 'NONE', 'WORKASPACE' ) );
#23265=ADVANCED_FACE ( 'NONE', ( #14295 ), #12510, .T. ) ;
#23283=DIRECTION ( 'NONE',  ( -1.000000000000000000, 0.000000000000000000, 0.000000000000000000 ) ) ;
#23293=DIRECTION ( 'NONE',  ( 1.000000000000000000, 0.000000000000000000, 0.000000000000000000 ) ) ;
#23299=ORIENTED_EDGE ( 'NONE', *, *, #22047, .T. ) ;
#23300=CIRCLE ( 'NONE', #14923, 8.749000000000004107 ) ;
#23306=DIRECTION ( 'NONE',  ( 0.000000000000000000, 0.000000000000000000, -1.000000000000000000 ) ) ;
#23307=CARTESIAN_POINT ( 'NONE',  ( 4.999999999999999112, -4.729683950898921907, 7.360373001730902587 ) ) ;
#23312=CARTESIAN_POINT ( 'NONE',  ( -20.00005080000000035, 0.000000000000000000, 0.000000000000000000 ) ) ;
#23320=ORIENTED_EDGE ( 'NONE', *, *, #23397, .T. ) ;
#23338=LINE ( 'NONE', #1286, #18706 ) ;
#23339=LINE ( 'NONE', #19857, #21364 ) ;
#23344=CIRCLE ( 'NONE', #7692, 11.00000000000000000 ) ;
#23356=CARTESIAN_POINT ( 'NONE',  ( 4.999999999999999112, 0.000000000000000000, 0.000000000000000000 ) ) ;
#23361=CARTESIAN_POINT ( 'NONE',  ( 4.999999999999999112, 0.000000000000000000, 0.000000000000000000 ) ) ;
#23363=DIRECTION ( 'NONE',  ( -1.000000000000000000, 0.000000000000000000, 0.000000000000000000 ) ) ;
#23369=ADVANCED_FACE ( 'NONE', ( #20112 ), #18692, .T. ) ;
#23374=CIRCLE ( 'NONE', #5788, 11.00000000000000000 ) ;
#23397=EDGE_CURVE ( 'NONE', #12130, #10244, #4222, .T. ) ;
#23401=ORIENTED_EDGE ( 'NONE', *, *, #615, .F. ) ;
#23406=SHAPE_REPRESENTATION_RELATIONSHIP ( 'NONE' , 'NONE' ,  #16640, #20459 ) ;
#23411=EDGE_CURVE ( 'NONE', #5926, #17904, #22151, .T. ) ;
#23415=DIRECTION ( 'NONE',  ( -1.000000000000000000, -0.000000000000000000, -0.000000000000000000 ) ) ;
#23427=ADVANCED_FACE ( 'NONE', ( #16787 ), #368, .T. ) ;
#23433=ORIENTED_EDGE ( 'NONE', *, *, #16015, .T. ) ;
#23436=CARTESIAN_POINT ( 'NONE',  ( 4.999999999999999112, -8.734705317681623171, -0.4999240074895356933 ) ) ;
#23440=CARTESIAN_POINT ( 'NONE',  ( 4.999999999999999112, -9.241976615262146311, -1.699438267350473097 ) ) ;
#23442=DIRECTION ( 'NONE',  ( 0.000000000000000000, 0.000000000000000000, 1.000000000000000000 ) ) ;
#23444=DIRECTION ( 'NONE',  ( -1.000000000000000000, 0.000000000000000000, 0.000000000000000000 ) ) ;
#23449=CARTESIAN_POINT ( 'NONE',  ( 4.999999999999999112, -2.223716399045513548, -8.461683424509336859 ) ) ;
#23456=DIRECTION ( 'NONE',  ( 0.000000000000000000, 0.000000000000000000, 1.000000000000000000 ) ) ;
#23470=VERTEX_POINT ( 'NONE', #11658 ) ;
#23481=FACE_OUTER_BOUND ( 'NONE', #22063, .T. ) ;
#23501=EDGE_CURVE ( 'NONE', #20516, #6311, #15245, .T. ) ;
#23507=DIRECTION ( 'NONE',  ( 0.000000000000000000, -0.9510565162951500895, -0.3090169943749582204 ) ) ;
#23514=VECTOR ( 'NONE', #14832, 1000.000000000000000 ) ;
#23517=CYLINDRICAL_SURFACE ( 'NONE', #8615, 11.00000000000000000 ) ;
#23523=AXIS2_PLACEMENT_3D ( 'NONE', #18530, #8137, #805 ) ;
#23533=EDGE_CURVE ( 'NONE', #17270, #22762, #5380, .T. ) ;
#23534=CARTESIAN_POINT ( 'NONE',  ( 0.000000000000000000, 4.057423117305393845, 8.475820894092990443 ) ) ;
#23536=ORIENTED_EDGE ( 'NONE', *, *, #723, .T. ) ;
#23538=CIRCLE ( 'NONE', #11333, 4.000000000000001776 ) ;
#23540=AXIS2_PLACEMENT_3D ( 'NONE', #11377, #18657, #2244 ) ;
#23543=CARTESIAN_POINT ( 'NONE',  ( 4.999999999999999112, 8.461683424509315543, 2.223716399045600145 ) ) ;
#23550=VECTOR ( 'NONE', #7042, 1000.000000000000000 ) ;
#23557=ORIENTED_EDGE ( 'NONE', *, *, #8449, .T. ) ;
#23559=AXIS2_PLACEMENT_3D ( 'NONE', #15255, #6011, #843 ) ;
#23571=DIRECTION ( 'NONE',  ( -1.000000000000000000, -0.000000000000000000, -0.000000000000000000 ) ) ;
#23575=EDGE_CURVE ( 'NONE', #9212, #9912, #5331, .T. ) ;
#23576=CARTESIAN_POINT ( 'NONE',  ( 2.499999999999999556, -1.975651141462315463, 10.82112760146735475 ) ) ;
#23590=ORIENTED_EDGE ( 'NONE', *, *, #13154, .T. ) ;
#23592=ORIENTED_EDGE ( 'NONE', *, *, #3095, .F. ) ;
#23593=CARTESIAN_POINT ( 'NONE',  ( 2.499999999999999556, 9.915734732513284300, -4.762163868918174892 ) ) ;
#23599=EDGE_CURVE ( 'NONE', #3988, #6515, #23344, .T. ) ;
#23601=AXIS2_PLACEMENT_3D ( 'NONE', #8538, #20954, #21078 ) ;
#23636=AXIS2_PLACEMENT_3D ( 'NONE', #5805, #12892, #7385 ) ;
#23640=ORIENTED_EDGE ( 'NONE', *, *, #22684, .T. ) ;
#23643=ORIENTED_EDGE ( 'NONE', *, *, #18915, .T. ) ;
#23661=AXIS2_PLACEMENT_3D ( 'NONE', #5369, #23571, #5482 ) ;
#23665=CARTESIAN_POINT ( 'NONE',  ( 0.000000000000000000, -0.4999240074895051067, 8.734705317681624948 ) ) ;
#23668=DIRECTION ( 'NONE',  ( 0.000000000000000000, 0.8090169943749446757, 0.5877852522924770229 ) ) ;
#23672=DIRECTION ( 'NONE',  ( -1.000000000000000000, -0.000000000000000000, -0.000000000000000000 ) ) ;
#23687=AXIS2_PLACEMENT_3D ( 'NONE', #13561, #22637, #9847 ) ;
ENDSEC;
END-ISO-10303-21;
